ISO-10303-21;
HEADER;
/* Generated by software containing ST-Developer
 * from STEP Tools, Inc. (www.steptools.com) 
 */

FILE_DESCRIPTION(
/* description */ (''),
/* implementation_level */ '2;1');

FILE_NAME(
/* name */ 'Hex nut M3.step',
/* time_stamp */ '2026-11-10T09:14:46-08:00',
/* author */ (''),
/* organization */ (''),
/* preprocessor_version */ 'ST-DEVELOPER v20.2',
/* originating_system */ 'Autodesk Translation Framework v15.17.0.0',
/* authorisation */ '');

FILE_SCHEMA (('AUTOMOTIVE_DESIGN { 1 0 10303 214 3 1 1 }'));
ENDSEC;

DATA;
#10=MECHANICAL_DESIGN_GEOMETRIC_PRESENTATION_REPRESENTATION('',(#566),#19471);
#170=B_SPLINE_SURFACE_WITH_KNOTS('',3,3,((#18842,#18843,#18844,#18845,#18846,
#18847,#18848,#18849,#18850,#18851,#18852,#18853,#18854,#18855,#18856,#18857,
#18858,#18859,#18860,#18861,#18862,#18863,#18864,#18865,#18866,#18867,#18868,
#18869,#18870,#18871,#18872,#18873,#18874,#18875,#18876,#18877),(#18878,
#18879,#18880,#18881,#18882,#18883,#18884,#18885,#18886,#18887,#18888,#18889,
#18890,#18891,#18892,#18893,#18894,#18895,#18896,#18897,#18898,#18899,#18900,
#18901,#18902,#18903,#18904,#18905,#18906,#18907,#18908,#18909,#18910,#18911,
#18912,#18913),(#18914,#18915,#18916,#18917,#18918,#18919,#18920,#18921,
#18922,#18923,#18924,#18925,#18926,#18927,#18928,#18929,#18930,#18931,#18932,
#18933,#18934,#18935,#18936,#18937,#18938,#18939,#18940,#18941,#18942,#18943,
#18944,#18945,#18946,#18947,#18948,#18949),(#18950,#18951,#18952,#18953,
#18954,#18955,#18956,#18957,#18958,#18959,#18960,#18961,#18962,#18963,#18964,
#18965,#18966,#18967,#18968,#18969,#18970,#18971,#18972,#18973,#18974,#18975,
#18976,#18977,#18978,#18979,#18980,#18981,#18982,#18983,#18984,#18985)),
 .UNSPECIFIED.,.F.,.F.,.F.,(4,4),(4,1,1,1,1,1,1,1,1,1,1,1,1,1,1,1,1,1,1,
1,1,1,1,1,1,1,1,1,1,1,1,1,1,4),(0.,0.0321584099938622),(11.8553612635794,
12.830508595889,13.8056559281987,14.7808032605084,15.755950592818,16.7310979251277,
17.7062452574374,18.681392589747,19.6565399220567,20.6316872543664,21.606834586676,
22.5819819189857,23.5571292512954,24.532276583605,25.5074239159147,26.4825712482243,
27.457718580534,28.4328659128437,29.4080132451533,30.383160577463,31.3583079097727,
32.3334552420823,33.308602574392,34.2837499067017,35.2588972390113,36.234044571321,
37.2091919036307,38.1843392359403,39.15948656825,40.1346339005596,41.1097812328693,
42.084928565179,43.0600758974886,44.0352232297983),.UNSPECIFIED.);
#171=B_SPLINE_SURFACE_WITH_KNOTS('',3,3,((#19109,#19110,#19111,#19112,#19113,
#19114,#19115,#19116,#19117,#19118,#19119,#19120,#19121,#19122,#19123,#19124,
#19125,#19126,#19127,#19128,#19129,#19130,#19131,#19132,#19133,#19134,#19135,
#19136,#19137,#19138,#19139,#19140,#19141,#19142,#19143,#19144),(#19145,
#19146,#19147,#19148,#19149,#19150,#19151,#19152,#19153,#19154,#19155,#19156,
#19157,#19158,#19159,#19160,#19161,#19162,#19163,#19164,#19165,#19166,#19167,
#19168,#19169,#19170,#19171,#19172,#19173,#19174,#19175,#19176,#19177,#19178,
#19179,#19180),(#19181,#19182,#19183,#19184,#19185,#19186,#19187,#19188,
#19189,#19190,#19191,#19192,#19193,#19194,#19195,#19196,#19197,#19198,#19199,
#19200,#19201,#19202,#19203,#19204,#19205,#19206,#19207,#19208,#19209,#19210,
#19211,#19212,#19213,#19214,#19215,#19216),(#19217,#19218,#19219,#19220,
#19221,#19222,#19223,#19224,#19225,#19226,#19227,#19228,#19229,#19230,#19231,
#19232,#19233,#19234,#19235,#19236,#19237,#19238,#19239,#19240,#19241,#19242,
#19243,#19244,#19245,#19246,#19247,#19248,#19249,#19250,#19251,#19252)),
 .UNSPECIFIED.,.F.,.F.,.F.,(4,4),(4,1,1,1,1,1,1,1,1,1,1,1,1,1,1,1,1,1,1,
1,1,1,1,1,1,1,1,1,1,1,1,1,1,4),(0.,0.0321584099938622),(14.3984001269719,
15.3735474592815,16.3486947915912,17.3238421239009,18.2989894562105,19.2741367885202,
20.2492841208299,21.2244314531395,22.1995787854492,23.1747261177589,24.1498734500685,
25.1250207823782,26.1001681146879,27.0753154469975,28.0504627793072,29.0256101116168,
30.0007574439265,30.9759047762362,31.9510521085458,32.9261994408555,33.9013467731652,
34.8764941054748,35.8516414377845,36.8267887700942,37.8019361024038,38.7770834347135,
39.7522307670232,40.7273780993328,41.7025254316425,42.6776727639522,43.6528200962618,
44.6279674285715,45.6031147608811,46.5782620931908),.UNSPECIFIED.);
#511=B_SPLINE_CURVE_WITH_KNOTS('',3,(#18512,#18513,#18514,#18515,#18516,
#18517,#18518),.UNSPECIFIED.,.F.,.F.,(4,3,4),(-30.159289474462,-29.2544199692899,
-28.9853432330879),.UNSPECIFIED.);
#512=B_SPLINE_CURVE_WITH_KNOTS('',3,(#18524,#18525,#18526,#18527,#18528,
#18529,#18530,#18531,#18532,#18533,#18534,#18535,#18536,#18537,#18538,#18539,
#18540,#18541,#18542),.UNSPECIFIED.,.F.,.F.,(4,3,3,3,3,3,4),(26.4423043696954,
27.3041253046706,28.2792726369803,29.25441996929,30.2295673015996,31.2047146339093,
32.179861966219),.UNSPECIFIED.);
#513=B_SPLINE_CURVE_WITH_KNOTS('',3,(#18544,#18545,#18546,#18547,#18548,
#18549,#18550,#18551,#18552,#18553,#18554,#18555,#18556,#18557,#18558,#18559,
#18560,#18561,#18562,#18563,#18564,#18565),.UNSPECIFIED.,.F.,.F.,(4,3,3,
3,3,3,3,4),(-28.9853432330879,-28.2792726369803,-27.3041253046706,-26.3289779723609,
-25.3538306400513,-24.3786833077416,-23.403535975432,-22.7021579259084),
 .UNSPECIFIED.);
#514=B_SPLINE_CURVE_WITH_KNOTS('',3,(#18570,#18571,#18572,#18573,#18574,
#18575,#18576,#18577,#18578,#18579,#18580,#18581,#18582,#18583,#18584,#18585,
#18586,#18587,#18588,#18589,#18590,#18591,#18592,#18593,#18594),
 .UNSPECIFIED.,.F.,.F.,(4,3,3,3,3,3,3,3,4),(20.1591190625159,20.478093978503,
21.4532413108126,22.4283886431223,23.403535975432,24.3786833077416,25.3538306400513,
26.328977972361,26.4423043696954),.UNSPECIFIED.);
#515=B_SPLINE_CURVE_WITH_KNOTS('',3,(#18595,#18596,#18597,#18598,#18599,
#18600,#18601,#18602,#18603,#18604,#18605,#18606,#18607,#18608,#18609,#18610,
#18611,#18612,#18613,#18614,#18615,#18616,#18617,#18618,#18619),
 .UNSPECIFIED.,.F.,.F.,(4,3,3,3,3,3,3,3,4),(-22.7021579259084,-22.4283886431223,
-21.4532413108126,-20.478093978503,-19.5029466461933,-18.5277993138836,
-17.552651981574,-16.5775046492643,-16.4189726187288),.UNSPECIFIED.);
#516=B_SPLINE_CURVE_WITH_KNOTS('',3,(#18624,#18625,#18626,#18627,#18628,
#18629,#18630,#18631,#18632,#18633,#18634,#18635,#18636,#18637,#18638,#18639,
#18640,#18641,#18642,#18643,#18644,#18645),.UNSPECIFIED.,.F.,.F.,(4,3,3,
3,3,3,3,4),(13.8759337553363,14.627209984645,15.6023573169546,16.5775046492643,
17.552651981574,18.5277993138836,19.5029466461933,20.1591190625159),
 .UNSPECIFIED.);
#517=B_SPLINE_CURVE_WITH_KNOTS('',3,(#18646,#18647,#18648,#18649,#18650,
#18651,#18652,#18653,#18654,#18655,#18656,#18657,#18658,#18659,#18660,#18661,
#18662,#18663,#18664,#18665,#18666,#18667),.UNSPECIFIED.,.F.,.F.,(4,3,3,
3,3,3,3,4),(-16.4189726187288,-15.6023573169546,-14.627209984645,-13.6520626523353,
-12.6769153200256,-11.701767987716,-10.7266206554063,-10.1357873115492),
 .UNSPECIFIED.);
#518=B_SPLINE_CURVE_WITH_KNOTS('',3,(#18673,#18674,#18675,#18676,#18677,
#18678,#18679,#18680,#18681,#18682,#18683,#18684,#18685),.UNSPECIFIED.,
 .F.,.F.,(4,3,3,3,4),(-3.8526020043696,-2.92544199692899,-1.95029466461933,
-0.975147332309664,0.),.UNSPECIFIED.);
#519=B_SPLINE_CURVE_WITH_KNOTS('',3,(#18688,#18689,#18690,#18691,#18692,
#18693,#18694,#18695,#18696,#18697,#18698,#18699,#18700,#18701,#18702,#18703,
#18704,#18705,#18706),.UNSPECIFIED.,.F.,.F.,(4,3,3,3,3,3,4),(2.02057249175693,
2.925441996929,3.90058932923866,4.87573666154832,5.85088399385799,6.82603132616766,
7.59274844815668),.UNSPECIFIED.);
#520=B_SPLINE_CURVE_WITH_KNOTS('',3,(#18712,#18713,#18714,#18715,#18716,
#18717,#18718),.UNSPECIFIED.,.F.,.F.,(4,1,1,1,4),(40.8407044966673,41.1097812328693,
42.084928565179,43.0600758974886,44.0352232297983),.UNSPECIFIED.);
#521=B_SPLINE_CURVE_WITH_KNOTS('',3,(#18721,#18722,#18723,#18724,#18725,
#18726,#18727),.UNSPECIFIED.,.F.,.F.,(4,1,1,1,4),(40.8407044966673,41.7025254316425,
42.6776727639522,43.6528200962618,44.5576896014339),.UNSPECIFIED.);
#522=B_SPLINE_CURVE_WITH_KNOTS('',3,(#18732,#18733,#18734,#18735,#18736,
#18737,#18738,#18739,#18740,#18741),.UNSPECIFIED.,.F.,.F.,(4,1,1,1,1,1,
1,4),(34.5575191894877,35.2588972390113,36.234044571321,37.2091919036307,
38.1843392359403,39.15948656825,40.1346339005596,40.8407044966673),
 .UNSPECIFIED.);
#523=B_SPLINE_CURVE_WITH_KNOTS('',3,(#18742,#18743,#18744,#18745,#18746,
#18747,#18748,#18749,#18750,#18751,#18752),.UNSPECIFIED.,.F.,.F.,(4,1,1,
1,1,1,1,1,4),(34.5575191894877,34.8764941054748,35.8516414377845,36.8267887700942,
37.8019361024038,38.7770834347135,39.7522307670232,40.7273780993328,40.8407044966673),
 .UNSPECIFIED.);
#524=B_SPLINE_CURVE_WITH_KNOTS('',3,(#18757,#18758,#18759,#18760,#18761,
#18762,#18763,#18764,#18765,#18766,#18767),.UNSPECIFIED.,.F.,.F.,(4,1,1,
1,1,1,1,1,4),(28.2743338823081,28.4328659128437,29.4080132451533,30.383160577463,
31.3583079097727,32.3334552420823,33.308602574392,34.2837499067017,34.5575191894877),
 .UNSPECIFIED.);
#525=B_SPLINE_CURVE_WITH_KNOTS('',3,(#18768,#18769,#18770,#18771,#18772,
#18773,#18774,#18775,#18776,#18777),.UNSPECIFIED.,.F.,.F.,(4,1,1,1,1,1,
1,4),(28.2743338823081,29.0256101116168,30.0007574439265,30.9759047762362,
31.9510521085458,32.9261994408555,33.9013467731652,34.5575191894877),
 .UNSPECIFIED.);
#526=B_SPLINE_CURVE_WITH_KNOTS('',3,(#18782,#18783,#18784,#18785,#18786,
#18787,#18788,#18789,#18790,#18791),.UNSPECIFIED.,.F.,.F.,(4,1,1,1,1,1,
1,4),(21.9911485751285,22.5819819189857,23.5571292512954,24.532276583605,
25.5074239159147,26.4825712482243,27.457718580534,28.2743338823081),
 .UNSPECIFIED.);
#527=B_SPLINE_CURVE_WITH_KNOTS('',3,(#18792,#18793,#18794,#18795,#18796,
#18797,#18798,#18799,#18800,#18801,#18802),.UNSPECIFIED.,.F.,.F.,(4,1,1,
1,1,1,1,1,4),(21.9911485751285,22.1995787854492,23.1747261177589,24.1498734500685,
25.1250207823782,26.1001681146879,27.0753154469975,28.0504627793072,28.2743338823081),
 .UNSPECIFIED.);
#528=B_SPLINE_CURVE_WITH_KNOTS('',3,(#18808,#18809,#18810,#18811,#18812),
 .UNSPECIFIED.,.F.,.F.,(4,1,4),(14.3984001269719,15.3735474592815,15.7079632679489),
 .UNSPECIFIED.);
#529=B_SPLINE_CURVE_WITH_KNOTS('',3,(#18815,#18816,#18817,#18818,#18819),
 .UNSPECIFIED.,.F.,.F.,(4,1,4),(13.8759337553363,14.7808032605084,15.7079632679489),
 .UNSPECIFIED.);
#530=B_SPLINE_CURVE_WITH_KNOTS('',3,(#18821,#18822,#18823,#18824,#18825,
#18826,#18827,#18828,#18829,#18830,#18831),.UNSPECIFIED.,.F.,.F.,(4,1,1,
1,1,1,1,1,4),(15.7079632679489,15.755950592818,16.7310979251277,17.7062452574374,
18.681392589747,19.6565399220567,20.6316872543664,21.606834586676,21.9911485751285),
 .UNSPECIFIED.);
#531=B_SPLINE_CURVE_WITH_KNOTS('',3,(#18832,#18833,#18834,#18835,#18836,
#18837,#18838,#18839,#18840,#18841),.UNSPECIFIED.,.F.,.F.,(4,1,1,1,1,1,
1,4),(15.7079632679489,16.3486947915912,17.3238421239009,18.2989894562105,
19.2741367885202,20.2492841208299,21.2244314531395,21.9911485751285),
 .UNSPECIFIED.);
#532=B_SPLINE_CURVE_WITH_KNOTS('',3,(#18986,#18987,#18988,#18989,#18990,
#18991,#18992,#18993,#18994,#18995,#18996,#18997,#18998,#18999,#19000,#19001,
#19002,#19003,#19004,#19005,#19006,#19007,#19008,#19009,#19010,#19011,#19012,
#19013,#19014,#19015,#19016,#19017,#19018,#19019,#19020,#19021,#19022,#19023,
#19024,#19025,#19026,#19027,#19028,#19029,#19030,#19031,#19032,#19033,#19034),
 .UNSPECIFIED.,.F.,.F.,(4,3,3,3,3,3,3,3,3,3,3,3,3,3,3,3,4),(0.,0.0320333804888866,
0.0505515708593653,0.0603413132804416,0.0917900141854983,0.108096115778005,
0.122914675479851,0.145143248337739,0.168151513577436,0.177516949333476,
0.202471322707608,0.21794283081622,0.231200110368267,0.247503117401854,
0.263651632124391,0.277334442830003,0.286347380332244),.UNSPECIFIED.);
#533=B_SPLINE_CURVE_WITH_KNOTS('',3,(#19035,#19036,#19037,#19038,#19039,
#19040,#19041,#19042,#19043,#19044,#19045,#19046,#19047,#19048,#19049,#19050,
#19051,#19052,#19053,#19054,#19055,#19056,#19057,#19058,#19059,#19060,#19061,
#19062,#19063,#19064,#19065,#19066,#19067,#19068,#19069,#19070,#19071,#19072,
#19073,#19074,#19075,#19076,#19077,#19078,#19079,#19080,#19081,#19082,#19083),
 .UNSPECIFIED.,.F.,.F.,(4,3,3,3,3,3,3,3,3,3,3,3,3,3,3,3,4),(0.,0.0274305464075637,
0.0492901149097146,0.0591933555873536,0.0887250095166089,0.100015570674795,
0.108381796308415,0.130826479038955,0.152531076563578,0.162815893631175,
0.190691958353668,0.212372986031639,0.222945305605857,0.245534254906135,
0.257847836118801,0.274320152521146,0.28514280399515),.UNSPECIFIED.);
#534=B_SPLINE_CURVE_WITH_KNOTS('',3,(#19084,#19085,#19086,#19087,#19088,
#19089,#19090,#19091,#19092,#19093,#19094,#19095,#19096,#19097,#19098,#19099,
#19100,#19101,#19102,#19103,#19104,#19105,#19106,#19107,#19108),
 .UNSPECIFIED.,.F.,.F.,(4,3,3,3,3,3,3,3,4),(-10.1357873115492,-9.75147332309665,
-8.77632599078699,-7.80117865847732,-6.82603132616766,-5.85088399385799,
-4.87573666154833,-3.90058932923866,-3.8526020043696),.UNSPECIFIED.);
#535=B_SPLINE_CURVE_WITH_KNOTS('',3,(#19253,#19254,#19255,#19256,#19257,
#19258,#19259,#19260,#19261,#19262,#19263,#19264,#19265,#19266,#19267,#19268,
#19269,#19270,#19271,#19272,#19273,#19274,#19275,#19276,#19277,#19278,#19279,
#19280,#19281,#19282,#19283,#19284,#19285,#19286,#19287,#19288,#19289,#19290,
#19291,#19292,#19293,#19294,#19295,#19296,#19297,#19298,#19299,#19300,#19301),
 .UNSPECIFIED.,.F.,.F.,(4,3,3,3,3,3,3,3,3,3,3,3,3,3,3,3,4),(0.,0.0274305890506951,
0.0492901290331875,0.0591933603491513,0.0887250177779717,0.100015607166709,
0.108381835831352,0.13082647903896,0.152531071764912,0.162815892251191,
0.190691957318683,0.212372984486691,0.22294529735758,0.245534140364172,
0.257847701250626,0.274320152521159,0.285142803995162),.UNSPECIFIED.);
#536=B_SPLINE_CURVE_WITH_KNOTS('',3,(#19302,#19303,#19304,#19305,#19306,
#19307,#19308,#19309,#19310,#19311,#19312,#19313,#19314,#19315,#19316,#19317,
#19318,#19319,#19320,#19321,#19322,#19323,#19324,#19325,#19326),
 .UNSPECIFIED.,.F.,.F.,(4,3,3,3,3,3,3,3,4),(7.59274844815668,7.80117865847732,
8.77632599078698,9.75147332309665,10.7266206554063,11.701767987716,12.6769153200256,
13.6520626523353,13.8759337553363),.UNSPECIFIED.);
#537=B_SPLINE_CURVE_WITH_KNOTS('',3,(#19327,#19328,#19329,#19330,#19331,
#19332,#19333,#19334,#19335,#19336,#19337,#19338,#19339,#19340,#19341,#19342,
#19343,#19344,#19345,#19346,#19347,#19348,#19349,#19350,#19351,#19352,#19353,
#19354,#19355,#19356,#19357,#19358,#19359,#19360,#19361,#19362,#19363,#19364,
#19365,#19366,#19367,#19368,#19369,#19370,#19371,#19372,#19373,#19374,#19375),
 .UNSPECIFIED.,.F.,.F.,(4,3,3,3,3,3,3,3,3,3,3,3,3,3,3,3,4),(0.,0.0320334058164849,
0.0505515938322513,0.0603413311462071,0.0917900214840119,0.108096111687201,
0.122914678304232,0.145143248337743,0.168151527562726,0.177516955081398,
0.202471327018552,0.217942288122009,0.231200024743484,0.24750284136614,
0.263651600306541,0.277334442830014,0.286347380332252),.UNSPECIFIED.);
#546=SHAPE_REPRESENTATION_RELATIONSHIP('SRR','None',#19526,#556);
#556=ADVANCED_BREP_SHAPE_REPRESENTATION('',(#576),#19469);
#566=STYLED_ITEM('',(#19586),#576);
#576=MANIFOLD_SOLID_BREP('Body1',#7159);
#649=FACE_BOUND('',#1693,.T.);
#650=FACE_BOUND('',#1702,.T.);
#810=PLANE('',#7785);
#811=PLANE('',#7787);
#812=PLANE('',#7788);
#813=PLANE('',#7789);
#814=PLANE('',#7790);
#815=PLANE('',#7791);
#816=PLANE('',#7792);
#817=PLANE('',#7793);
#1203=FACE_OUTER_BOUND('',#1679,.T.);
#1204=FACE_OUTER_BOUND('',#1680,.T.);
#1205=FACE_OUTER_BOUND('',#1681,.T.);
#1206=FACE_OUTER_BOUND('',#1682,.T.);
#1207=FACE_OUTER_BOUND('',#1683,.T.);
#1208=FACE_OUTER_BOUND('',#1684,.T.);
#1209=FACE_OUTER_BOUND('',#1685,.T.);
#1210=FACE_OUTER_BOUND('',#1686,.T.);
#1211=FACE_OUTER_BOUND('',#1687,.T.);
#1212=FACE_OUTER_BOUND('',#1688,.T.);
#1213=FACE_OUTER_BOUND('',#1689,.T.);
#1214=FACE_OUTER_BOUND('',#1690,.T.);
#1215=FACE_OUTER_BOUND('',#1691,.T.);
#1216=FACE_OUTER_BOUND('',#1692,.T.);
#1217=FACE_OUTER_BOUND('',#1694,.T.);
#1218=FACE_OUTER_BOUND('',#1695,.T.);
#1219=FACE_OUTER_BOUND('',#1696,.T.);
#1220=FACE_OUTER_BOUND('',#1697,.T.);
#1221=FACE_OUTER_BOUND('',#1698,.T.);
#1222=FACE_OUTER_BOUND('',#1699,.T.);
#1223=FACE_OUTER_BOUND('',#1700,.T.);
#1224=FACE_OUTER_BOUND('',#1701,.T.);
#1679=EDGE_LOOP('',(#6469,#6470,#6471));
#1680=EDGE_LOOP('',(#6472,#6473,#6474,#6475,#6476));
#1681=EDGE_LOOP('',(#6477,#6478,#6479,#6480));
#1682=EDGE_LOOP('',(#6481,#6482,#6483,#6484));
#1683=EDGE_LOOP('',(#6485,#6486,#6487,#6488));
#1684=EDGE_LOOP('',(#6489,#6490,#6491,#6492));
#1685=EDGE_LOOP('',(#6493,#6494,#6495,#6496));
#1686=EDGE_LOOP('',(#6497,#6498,#6499,#6500));
#1687=EDGE_LOOP('',(#6501,#6502,#6503,#6504));
#1688=EDGE_LOOP('',(#6505,#6506,#6507,#6508));
#1689=EDGE_LOOP('',(#6509,#6510,#6511,#6512));
#1690=EDGE_LOOP('',(#6513,#6514,#6515,#6516,#6517,#6518,#6519,#6520,#6521,
#6522,#6523,#6524,#6525,#6526));
#1691=EDGE_LOOP('',(#6527,#6528,#6529,#6530,#6531,#6532,#6533,#6534,#6535,
#6536,#6537,#6538,#6539));
#1692=EDGE_LOOP('',(#6540,#6541,#6542,#6543,#6544,#6545));
#1693=EDGE_LOOP('',(#6546,#6547,#6548,#6549));
#1694=EDGE_LOOP('',(#6550,#6551,#6552,#6553));
#1695=EDGE_LOOP('',(#6554,#6555,#6556,#6557));
#1696=EDGE_LOOP('',(#6558,#6559,#6560,#6561));
#1697=EDGE_LOOP('',(#6562,#6563,#6564,#6565));
#1698=EDGE_LOOP('',(#6566,#6567,#6568,#6569));
#1699=EDGE_LOOP('',(#6570,#6571,#6572,#6573));
#1700=EDGE_LOOP('',(#6574,#6575,#6576,#6577));
#1701=EDGE_LOOP('',(#6578,#6579,#6580,#6581,#6582,#6583));
#1702=EDGE_LOOP('',(#6584,#6585,#6586,#6587,#6588));
#2153=LINE('',#18509,#2627);
#2154=LINE('',#18522,#2628);
#2155=LINE('',#18569,#2629);
#2156=LINE('',#18623,#2630);
#2157=LINE('',#18671,#2631);
#2158=LINE('',#18710,#2632);
#2159=LINE('',#18731,#2633);
#2160=LINE('',#18756,#2634);
#2161=LINE('',#18781,#2635);
#2162=LINE('',#18806,#2636);
#2163=LINE('',#19379,#2637);
#2164=LINE('',#19381,#2638);
#2165=LINE('',#19383,#2639);
#2166=LINE('',#19385,#2640);
#2167=LINE('',#19387,#2641);
#2168=LINE('',#19388,#2642);
#2169=LINE('',#19393,#2643);
#2170=LINE('',#19394,#2644);
#2171=LINE('',#19395,#2645);
#2172=LINE('',#19398,#2646);
#2173=LINE('',#19399,#2647);
#2174=LINE('',#19402,#2648);
#2175=LINE('',#19403,#2649);
#2176=LINE('',#19406,#2650);
#2177=LINE('',#19407,#2651);
#2178=LINE('',#19410,#2652);
#2179=LINE('',#19411,#2653);
#2180=LINE('',#19413,#2654);
#2627=VECTOR('',#9259,0.15);
#2628=VECTOR('',#9264,0.15);
#2629=VECTOR('',#9269,0.15);
#2630=VECTOR('',#9272,0.15);
#2631=VECTOR('',#9275,0.15);
#2632=VECTOR('',#9280,0.1543);
#2633=VECTOR('',#9285,0.1543);
#2634=VECTOR('',#9288,0.1543);
#2635=VECTOR('',#9291,0.1543);
#2636=VECTOR('',#9294,0.1543);
#2637=VECTOR('',#9301,1.);
#2638=VECTOR('',#9302,1.);
#2639=VECTOR('',#9303,1.);
#2640=VECTOR('',#9304,1.);
#2641=VECTOR('',#9305,1.);
#2642=VECTOR('',#9306,1.);
#2643=VECTOR('',#9311,1.);
#2644=VECTOR('',#9312,1.);
#2645=VECTOR('',#9313,1.);
#2646=VECTOR('',#9316,1.);
#2647=VECTOR('',#9317,1.);
#2648=VECTOR('',#9320,1.);
#2649=VECTOR('',#9321,1.);
#2650=VECTOR('',#9324,1.);
#2651=VECTOR('',#9325,1.);
#2652=VECTOR('',#9328,1.);
#2653=VECTOR('',#9329,1.);
#2654=VECTOR('',#9332,1.);
#2838=CIRCLE('',#7770,0.12645);
#2839=CIRCLE('',#7772,0.12645);
#2840=CIRCLE('',#7776,0.12645);
#2841=CIRCLE('',#7778,0.1543);
#2842=CIRCLE('',#7783,0.1543);
#3467=VERTEX_POINT('',#18507);
#3468=VERTEX_POINT('',#18508);
#3469=VERTEX_POINT('',#18510);
#3470=VERTEX_POINT('',#18520);
#3471=VERTEX_POINT('',#18521);
#3472=VERTEX_POINT('',#18523);
#3473=VERTEX_POINT('',#18567);
#3474=VERTEX_POINT('',#18568);
#3475=VERTEX_POINT('',#18621);
#3476=VERTEX_POINT('',#18622);
#3477=VERTEX_POINT('',#18669);
#3478=VERTEX_POINT('',#18670);
#3479=VERTEX_POINT('',#18672);
#3480=VERTEX_POINT('',#18686);
#3481=VERTEX_POINT('',#18708);
#3482=VERTEX_POINT('',#18709);
#3483=VERTEX_POINT('',#18711);
#3484=VERTEX_POINT('',#18719);
#3485=VERTEX_POINT('',#18729);
#3486=VERTEX_POINT('',#18730);
#3487=VERTEX_POINT('',#18754);
#3488=VERTEX_POINT('',#18755);
#3489=VERTEX_POINT('',#18779);
#3490=VERTEX_POINT('',#18780);
#3491=VERTEX_POINT('',#18804);
#3492=VERTEX_POINT('',#18805);
#3493=VERTEX_POINT('',#18807);
#3494=VERTEX_POINT('',#18813);
#3495=VERTEX_POINT('',#19377);
#3496=VERTEX_POINT('',#19378);
#3497=VERTEX_POINT('',#19380);
#3498=VERTEX_POINT('',#19382);
#3499=VERTEX_POINT('',#19384);
#3500=VERTEX_POINT('',#19386);
#3501=VERTEX_POINT('',#19391);
#3502=VERTEX_POINT('',#19392);
#3503=VERTEX_POINT('',#19397);
#3504=VERTEX_POINT('',#19401);
#3505=VERTEX_POINT('',#19405);
#3506=VERTEX_POINT('',#19409);
#4475=EDGE_CURVE('',#3467,#3468,#2153,.T.);
#4476=EDGE_CURVE('',#3469,#3468,#2838,.F.);
#4477=EDGE_CURVE('',#3469,#3467,#511,.T.);
#4478=EDGE_CURVE('',#3470,#3471,#2154,.T.);
#4479=EDGE_CURVE('',#3471,#3472,#512,.T.);
#4480=EDGE_CURVE('',#3468,#3472,#2839,.F.);
#4481=EDGE_CURVE('',#3467,#3470,#513,.T.);
#4482=EDGE_CURVE('',#3473,#3474,#2155,.T.);
#4483=EDGE_CURVE('',#3474,#3471,#514,.T.);
#4484=EDGE_CURVE('',#3470,#3473,#515,.T.);
#4485=EDGE_CURVE('',#3475,#3476,#2156,.T.);
#4486=EDGE_CURVE('',#3476,#3474,#516,.T.);
#4487=EDGE_CURVE('',#3473,#3475,#517,.T.);
#4488=EDGE_CURVE('',#3477,#3478,#2157,.T.);
#4489=EDGE_CURVE('',#3477,#3479,#518,.T.);
#4490=EDGE_CURVE('',#3480,#3479,#2840,.T.);
#4491=EDGE_CURVE('',#3480,#3478,#519,.T.);
#4492=EDGE_CURVE('',#3481,#3482,#2158,.T.);
#4493=EDGE_CURVE('',#3482,#3483,#520,.T.);
#4494=EDGE_CURVE('',#3484,#3483,#2841,.T.);
#4495=EDGE_CURVE('',#3481,#3484,#521,.T.);
#4496=EDGE_CURVE('',#3485,#3486,#2159,.T.);
#4497=EDGE_CURVE('',#3486,#3482,#522,.T.);
#4498=EDGE_CURVE('',#3485,#3481,#523,.T.);
#4499=EDGE_CURVE('',#3487,#3488,#2160,.T.);
#4500=EDGE_CURVE('',#3488,#3486,#524,.T.);
#4501=EDGE_CURVE('',#3487,#3485,#525,.T.);
#4502=EDGE_CURVE('',#3489,#3490,#2161,.T.);
#4503=EDGE_CURVE('',#3490,#3488,#526,.T.);
#4504=EDGE_CURVE('',#3489,#3487,#527,.T.);
#4505=EDGE_CURVE('',#3491,#3492,#2162,.T.);
#4506=EDGE_CURVE('',#3493,#3491,#528,.T.);
#4507=EDGE_CURVE('',#3494,#3493,#2842,.T.);
#4508=EDGE_CURVE('',#3494,#3492,#529,.T.);
#4509=EDGE_CURVE('',#3492,#3490,#530,.T.);
#4510=EDGE_CURVE('',#3491,#3489,#531,.T.);
#4511=EDGE_CURVE('',#3483,#3469,#532,.T.);
#4512=EDGE_CURVE('',#3479,#3494,#533,.T.);
#4513=EDGE_CURVE('',#3475,#3477,#534,.T.);
#4514=EDGE_CURVE('',#3472,#3484,#535,.T.);
#4515=EDGE_CURVE('',#3478,#3476,#536,.T.);
#4516=EDGE_CURVE('',#3493,#3480,#537,.T.);
#4517=EDGE_CURVE('',#3495,#3496,#2163,.T.);
#4518=EDGE_CURVE('',#3496,#3497,#2164,.T.);
#4519=EDGE_CURVE('',#3497,#3498,#2165,.T.);
#4520=EDGE_CURVE('',#3498,#3499,#2166,.T.);
#4521=EDGE_CURVE('',#3499,#3500,#2167,.T.);
#4522=EDGE_CURVE('',#3500,#3495,#2168,.T.);
#4523=EDGE_CURVE('',#3501,#3502,#2169,.T.);
#4524=EDGE_CURVE('',#3502,#3495,#2170,.T.);
#4525=EDGE_CURVE('',#3501,#3500,#2171,.T.);
#4526=EDGE_CURVE('',#3503,#3501,#2172,.T.);
#4527=EDGE_CURVE('',#3503,#3499,#2173,.T.);
#4528=EDGE_CURVE('',#3504,#3503,#2174,.T.);
#4529=EDGE_CURVE('',#3504,#3498,#2175,.T.);
#4530=EDGE_CURVE('',#3505,#3504,#2176,.T.);
#4531=EDGE_CURVE('',#3505,#3497,#2177,.T.);
#4532=EDGE_CURVE('',#3506,#3505,#2178,.T.);
#4533=EDGE_CURVE('',#3506,#3496,#2179,.T.);
#4534=EDGE_CURVE('',#3502,#3506,#2180,.T.);
#6469=ORIENTED_EDGE('',*,*,#4475,.T.);
#6470=ORIENTED_EDGE('',*,*,#4476,.F.);
#6471=ORIENTED_EDGE('',*,*,#4477,.T.);
#6472=ORIENTED_EDGE('',*,*,#4478,.T.);
#6473=ORIENTED_EDGE('',*,*,#4479,.T.);
#6474=ORIENTED_EDGE('',*,*,#4480,.F.);
#6475=ORIENTED_EDGE('',*,*,#4475,.F.);
#6476=ORIENTED_EDGE('',*,*,#4481,.T.);
#6477=ORIENTED_EDGE('',*,*,#4482,.T.);
#6478=ORIENTED_EDGE('',*,*,#4483,.T.);
#6479=ORIENTED_EDGE('',*,*,#4478,.F.);
#6480=ORIENTED_EDGE('',*,*,#4484,.T.);
#6481=ORIENTED_EDGE('',*,*,#4485,.T.);
#6482=ORIENTED_EDGE('',*,*,#4486,.T.);
#6483=ORIENTED_EDGE('',*,*,#4482,.F.);
#6484=ORIENTED_EDGE('',*,*,#4487,.T.);
#6485=ORIENTED_EDGE('',*,*,#4488,.F.);
#6486=ORIENTED_EDGE('',*,*,#4489,.T.);
#6487=ORIENTED_EDGE('',*,*,#4490,.F.);
#6488=ORIENTED_EDGE('',*,*,#4491,.T.);
#6489=ORIENTED_EDGE('',*,*,#4492,.T.);
#6490=ORIENTED_EDGE('',*,*,#4493,.T.);
#6491=ORIENTED_EDGE('',*,*,#4494,.F.);
#6492=ORIENTED_EDGE('',*,*,#4495,.F.);
#6493=ORIENTED_EDGE('',*,*,#4496,.T.);
#6494=ORIENTED_EDGE('',*,*,#4497,.T.);
#6495=ORIENTED_EDGE('',*,*,#4492,.F.);
#6496=ORIENTED_EDGE('',*,*,#4498,.F.);
#6497=ORIENTED_EDGE('',*,*,#4499,.T.);
#6498=ORIENTED_EDGE('',*,*,#4500,.T.);
#6499=ORIENTED_EDGE('',*,*,#4496,.F.);
#6500=ORIENTED_EDGE('',*,*,#4501,.F.);
#6501=ORIENTED_EDGE('',*,*,#4502,.T.);
#6502=ORIENTED_EDGE('',*,*,#4503,.T.);
#6503=ORIENTED_EDGE('',*,*,#4499,.F.);
#6504=ORIENTED_EDGE('',*,*,#4504,.F.);
#6505=ORIENTED_EDGE('',*,*,#4505,.F.);
#6506=ORIENTED_EDGE('',*,*,#4506,.F.);
#6507=ORIENTED_EDGE('',*,*,#4507,.F.);
#6508=ORIENTED_EDGE('',*,*,#4508,.T.);
#6509=ORIENTED_EDGE('',*,*,#4505,.T.);
#6510=ORIENTED_EDGE('',*,*,#4509,.T.);
#6511=ORIENTED_EDGE('',*,*,#4502,.F.);
#6512=ORIENTED_EDGE('',*,*,#4510,.F.);
#6513=ORIENTED_EDGE('',*,*,#4511,.F.);
#6514=ORIENTED_EDGE('',*,*,#4493,.F.);
#6515=ORIENTED_EDGE('',*,*,#4497,.F.);
#6516=ORIENTED_EDGE('',*,*,#4500,.F.);
#6517=ORIENTED_EDGE('',*,*,#4503,.F.);
#6518=ORIENTED_EDGE('',*,*,#4509,.F.);
#6519=ORIENTED_EDGE('',*,*,#4508,.F.);
#6520=ORIENTED_EDGE('',*,*,#4512,.F.);
#6521=ORIENTED_EDGE('',*,*,#4489,.F.);
#6522=ORIENTED_EDGE('',*,*,#4513,.F.);
#6523=ORIENTED_EDGE('',*,*,#4487,.F.);
#6524=ORIENTED_EDGE('',*,*,#4484,.F.);
#6525=ORIENTED_EDGE('',*,*,#4481,.F.);
#6526=ORIENTED_EDGE('',*,*,#4477,.F.);
#6527=ORIENTED_EDGE('',*,*,#4514,.F.);
#6528=ORIENTED_EDGE('',*,*,#4479,.F.);
#6529=ORIENTED_EDGE('',*,*,#4483,.F.);
#6530=ORIENTED_EDGE('',*,*,#4486,.F.);
#6531=ORIENTED_EDGE('',*,*,#4515,.F.);
#6532=ORIENTED_EDGE('',*,*,#4491,.F.);
#6533=ORIENTED_EDGE('',*,*,#4516,.F.);
#6534=ORIENTED_EDGE('',*,*,#4506,.T.);
#6535=ORIENTED_EDGE('',*,*,#4510,.T.);
#6536=ORIENTED_EDGE('',*,*,#4504,.T.);
#6537=ORIENTED_EDGE('',*,*,#4501,.T.);
#6538=ORIENTED_EDGE('',*,*,#4498,.T.);
#6539=ORIENTED_EDGE('',*,*,#4495,.T.);
#6540=ORIENTED_EDGE('',*,*,#4517,.T.);
#6541=ORIENTED_EDGE('',*,*,#4518,.T.);
#6542=ORIENTED_EDGE('',*,*,#4519,.T.);
#6543=ORIENTED_EDGE('',*,*,#4520,.T.);
#6544=ORIENTED_EDGE('',*,*,#4521,.T.);
#6545=ORIENTED_EDGE('',*,*,#4522,.T.);
#6546=ORIENTED_EDGE('',*,*,#4512,.T.);
#6547=ORIENTED_EDGE('',*,*,#4507,.T.);
#6548=ORIENTED_EDGE('',*,*,#4516,.T.);
#6549=ORIENTED_EDGE('',*,*,#4490,.T.);
#6550=ORIENTED_EDGE('',*,*,#4488,.T.);
#6551=ORIENTED_EDGE('',*,*,#4515,.T.);
#6552=ORIENTED_EDGE('',*,*,#4485,.F.);
#6553=ORIENTED_EDGE('',*,*,#4513,.T.);
#6554=ORIENTED_EDGE('',*,*,#4523,.T.);
#6555=ORIENTED_EDGE('',*,*,#4524,.T.);
#6556=ORIENTED_EDGE('',*,*,#4522,.F.);
#6557=ORIENTED_EDGE('',*,*,#4525,.F.);
#6558=ORIENTED_EDGE('',*,*,#4526,.T.);
#6559=ORIENTED_EDGE('',*,*,#4525,.T.);
#6560=ORIENTED_EDGE('',*,*,#4521,.F.);
#6561=ORIENTED_EDGE('',*,*,#4527,.F.);
#6562=ORIENTED_EDGE('',*,*,#4528,.T.);
#6563=ORIENTED_EDGE('',*,*,#4527,.T.);
#6564=ORIENTED_EDGE('',*,*,#4520,.F.);
#6565=ORIENTED_EDGE('',*,*,#4529,.F.);
#6566=ORIENTED_EDGE('',*,*,#4530,.T.);
#6567=ORIENTED_EDGE('',*,*,#4529,.T.);
#6568=ORIENTED_EDGE('',*,*,#4519,.F.);
#6569=ORIENTED_EDGE('',*,*,#4531,.F.);
#6570=ORIENTED_EDGE('',*,*,#4532,.T.);
#6571=ORIENTED_EDGE('',*,*,#4531,.T.);
#6572=ORIENTED_EDGE('',*,*,#4518,.F.);
#6573=ORIENTED_EDGE('',*,*,#4533,.F.);
#6574=ORIENTED_EDGE('',*,*,#4534,.T.);
#6575=ORIENTED_EDGE('',*,*,#4533,.T.);
#6576=ORIENTED_EDGE('',*,*,#4517,.F.);
#6577=ORIENTED_EDGE('',*,*,#4524,.F.);
#6578=ORIENTED_EDGE('',*,*,#4534,.F.);
#6579=ORIENTED_EDGE('',*,*,#4523,.F.);
#6580=ORIENTED_EDGE('',*,*,#4526,.F.);
#6581=ORIENTED_EDGE('',*,*,#4528,.F.);
#6582=ORIENTED_EDGE('',*,*,#4530,.F.);
#6583=ORIENTED_EDGE('',*,*,#4532,.F.);
#6584=ORIENTED_EDGE('',*,*,#4511,.T.);
#6585=ORIENTED_EDGE('',*,*,#4476,.T.);
#6586=ORIENTED_EDGE('',*,*,#4480,.T.);
#6587=ORIENTED_EDGE('',*,*,#4514,.T.);
#6588=ORIENTED_EDGE('',*,*,#4494,.T.);
#6728=CYLINDRICAL_SURFACE('',#7769,0.12645);
#6729=CYLINDRICAL_SURFACE('',#7771,0.12645);
#6730=CYLINDRICAL_SURFACE('',#7773,0.12645);
#6731=CYLINDRICAL_SURFACE('',#7774,0.12645);
#6732=CYLINDRICAL_SURFACE('',#7775,0.12645);
#6733=CYLINDRICAL_SURFACE('',#7777,0.1543);
#6734=CYLINDRICAL_SURFACE('',#7779,0.1543);
#6735=CYLINDRICAL_SURFACE('',#7780,0.1543);
#6736=CYLINDRICAL_SURFACE('',#7781,0.1543);
#6737=CYLINDRICAL_SURFACE('',#7782,0.1543);
#6738=CYLINDRICAL_SURFACE('',#7784,0.1543);
#6739=CYLINDRICAL_SURFACE('',#7786,0.12645);
#7125=ADVANCED_FACE('',(#1203),#6728,.F.);
#7126=ADVANCED_FACE('',(#1204),#6729,.F.);
#7127=ADVANCED_FACE('',(#1205),#6730,.F.);
#7128=ADVANCED_FACE('',(#1206),#6731,.F.);
#7129=ADVANCED_FACE('',(#1207),#6732,.F.);
#7130=ADVANCED_FACE('',(#1208),#6733,.F.);
#7131=ADVANCED_FACE('',(#1209),#6734,.F.);
#7132=ADVANCED_FACE('',(#1210),#6735,.F.);
#7133=ADVANCED_FACE('',(#1211),#6736,.F.);
#7134=ADVANCED_FACE('',(#1212),#6737,.F.);
#7135=ADVANCED_FACE('',(#1213),#6738,.F.);
#7136=ADVANCED_FACE('',(#1214),#170,.F.);
#7137=ADVANCED_FACE('',(#1215),#171,.F.);
#7138=ADVANCED_FACE('',(#1216,#649),#810,.T.);
#7139=ADVANCED_FACE('',(#1217),#6739,.F.);
#7140=ADVANCED_FACE('',(#1218),#811,.T.);
#7141=ADVANCED_FACE('',(#1219),#812,.T.);
#7142=ADVANCED_FACE('',(#1220),#813,.T.);
#7143=ADVANCED_FACE('',(#1221),#814,.T.);
#7144=ADVANCED_FACE('',(#1222),#815,.T.);
#7145=ADVANCED_FACE('',(#1223),#816,.T.);
#7146=ADVANCED_FACE('',(#1224,#650),#817,.F.);
#7159=CLOSED_SHELL('',(#7125,#7126,#7127,#7128,#7129,#7130,#7131,#7132,
#7133,#7134,#7135,#7136,#7137,#7138,#7139,#7140,#7141,#7142,#7143,#7144,
#7145,#7146));
#7768=AXIS2_PLACEMENT_3D('',#18505,#9255,#9256);
#7769=AXIS2_PLACEMENT_3D('',#18506,#9257,#9258);
#7770=AXIS2_PLACEMENT_3D('',#18511,#9260,#9261);
#7771=AXIS2_PLACEMENT_3D('',#18519,#9262,#9263);
#7772=AXIS2_PLACEMENT_3D('',#18543,#9265,#9266);
#7773=AXIS2_PLACEMENT_3D('',#18566,#9267,#9268);
#7774=AXIS2_PLACEMENT_3D('',#18620,#9270,#9271);
#7775=AXIS2_PLACEMENT_3D('',#18668,#9273,#9274);
#7776=AXIS2_PLACEMENT_3D('',#18687,#9276,#9277);
#7777=AXIS2_PLACEMENT_3D('',#18707,#9278,#9279);
#7778=AXIS2_PLACEMENT_3D('',#18720,#9281,#9282);
#7779=AXIS2_PLACEMENT_3D('',#18728,#9283,#9284);
#7780=AXIS2_PLACEMENT_3D('',#18753,#9286,#9287);
#7781=AXIS2_PLACEMENT_3D('',#18778,#9289,#9290);
#7782=AXIS2_PLACEMENT_3D('',#18803,#9292,#9293);
#7783=AXIS2_PLACEMENT_3D('',#18814,#9295,#9296);
#7784=AXIS2_PLACEMENT_3D('',#18820,#9297,#9298);
#7785=AXIS2_PLACEMENT_3D('',#19376,#9299,#9300);
#7786=AXIS2_PLACEMENT_3D('',#19389,#9307,#9308);
#7787=AXIS2_PLACEMENT_3D('',#19390,#9309,#9310);
#7788=AXIS2_PLACEMENT_3D('',#19396,#9314,#9315);
#7789=AXIS2_PLACEMENT_3D('',#19400,#9318,#9319);
#7790=AXIS2_PLACEMENT_3D('',#19404,#9322,#9323);
#7791=AXIS2_PLACEMENT_3D('',#19408,#9326,#9327);
#7792=AXIS2_PLACEMENT_3D('',#19412,#9330,#9331);
#7793=AXIS2_PLACEMENT_3D('',#19414,#9333,#9334);
#9255=DIRECTION('axis',(0.,0.,1.));
#9256=DIRECTION('refdir',(1.,0.,0.));
#9257=DIRECTION('center_axis',(0.,0.,-1.));
#9258=DIRECTION('ref_axis',(1.,0.,0.));
#9259=DIRECTION('',(0.,0.,-1.));
#9260=DIRECTION('center_axis',(0.,0.,-1.));
#9261=DIRECTION('ref_axis',(1.,0.,0.));
#9262=DIRECTION('center_axis',(0.,0.,-1.));
#9263=DIRECTION('ref_axis',(1.,0.,0.));
#9264=DIRECTION('',(0.,0.,-1.));
#9265=DIRECTION('center_axis',(0.,0.,-1.));
#9266=DIRECTION('ref_axis',(1.,0.,0.));
#9267=DIRECTION('center_axis',(0.,0.,-1.));
#9268=DIRECTION('ref_axis',(1.,0.,0.));
#9269=DIRECTION('',(0.,0.,-1.));
#9270=DIRECTION('center_axis',(0.,0.,-1.));
#9271=DIRECTION('ref_axis',(1.,0.,0.));
#9272=DIRECTION('',(0.,0.,-1.));
#9273=DIRECTION('center_axis',(0.,0.,-1.));
#9274=DIRECTION('ref_axis',(0.937385399639056,-0.348293859468591,0.));
#9275=DIRECTION('',(0.,0.,-1.));
#9276=DIRECTION('center_axis',(0.,0.,-1.));
#9277=DIRECTION('ref_axis',(1.,0.,0.));
#9278=DIRECTION('center_axis',(0.,0.,-1.));
#9279=DIRECTION('ref_axis',(0.28361887368566,0.958937085782627,0.));
#9280=DIRECTION('',(1.22464679914735E-16,8.07419868282478E-31,-1.));
#9281=DIRECTION('center_axis',(0.,0.,1.));
#9282=DIRECTION('ref_axis',(1.,6.71554824363804E-15,0.));
#9283=DIRECTION('center_axis',(0.,0.,-1.));
#9284=DIRECTION('ref_axis',(1.,6.71554824363804E-15,0.));
#9285=DIRECTION('',(1.22464679914735E-16,8.07419868282478E-31,-1.));
#9286=DIRECTION('center_axis',(0.,0.,-1.));
#9287=DIRECTION('ref_axis',(1.,6.71554824363804E-15,0.));
#9288=DIRECTION('',(1.22464679914735E-16,8.07419868282478E-31,-1.));
#9289=DIRECTION('center_axis',(0.,0.,-1.));
#9290=DIRECTION('ref_axis',(1.,6.71554824363804E-15,0.));
#9291=DIRECTION('',(1.22464679914735E-16,8.07419868282478E-31,-1.));
#9292=DIRECTION('center_axis',(0.,0.,-1.));
#9293=DIRECTION('ref_axis',(-0.60895050335979,-0.793208222636313,0.));
#9294=DIRECTION('',(1.22464679914735E-16,8.07419868282478E-31,-1.));
#9295=DIRECTION('center_axis',(0.,0.,-1.));
#9296=DIRECTION('ref_axis',(1.,6.71554824363804E-15,0.));
#9297=DIRECTION('center_axis',(0.,0.,-1.));
#9298=DIRECTION('ref_axis',(1.,6.71554824363804E-15,0.));
#9299=DIRECTION('center_axis',(0.,0.,1.));
#9300=DIRECTION('ref_axis',(1.,0.,0.));
#9301=DIRECTION('',(0.5,0.866025403784439,0.));
#9302=DIRECTION('',(-0.5,0.866025403784439,0.));
#9303=DIRECTION('',(-1.,0.,0.));
#9304=DIRECTION('',(-0.5,-0.866025403784439,0.));
#9305=DIRECTION('',(0.5,-0.866025403784439,0.));
#9306=DIRECTION('',(1.,-3.49629579342466E-16,0.));
#9307=DIRECTION('center_axis',(0.,0.,-1.));
#9308=DIRECTION('ref_axis',(1.,0.,0.));
#9309=DIRECTION('center_axis',(-3.49629579342466E-16,-1.,0.));
#9310=DIRECTION('ref_axis',(1.,-3.49629579342466E-16,0.));
#9311=DIRECTION('',(1.,-3.49629579342466E-16,0.));
#9312=DIRECTION('',(0.,0.,1.));
#9313=DIRECTION('',(0.,0.,1.));
#9314=DIRECTION('center_axis',(-0.866025403784439,-0.5,0.));
#9315=DIRECTION('ref_axis',(0.5,-0.866025403784439,0.));
#9316=DIRECTION('',(0.5,-0.866025403784439,0.));
#9317=DIRECTION('',(0.,0.,1.));
#9318=DIRECTION('center_axis',(-0.866025403784439,0.5,0.));
#9319=DIRECTION('ref_axis',(-0.5,-0.866025403784439,0.));
#9320=DIRECTION('',(-0.5,-0.866025403784439,0.));
#9321=DIRECTION('',(0.,0.,1.));
#9322=DIRECTION('center_axis',(0.,1.,0.));
#9323=DIRECTION('ref_axis',(-1.,0.,0.));
#9324=DIRECTION('',(-1.,0.,0.));
#9325=DIRECTION('',(0.,0.,1.));
#9326=DIRECTION('center_axis',(0.866025403784439,0.5,0.));
#9327=DIRECTION('ref_axis',(-0.5,0.866025403784439,0.));
#9328=DIRECTION('',(-0.5,0.866025403784439,0.));
#9329=DIRECTION('',(0.,0.,1.));
#9330=DIRECTION('center_axis',(0.866025403784439,-0.5,0.));
#9331=DIRECTION('ref_axis',(0.5,0.866025403784439,0.));
#9332=DIRECTION('',(0.5,0.866025403784439,0.));
#9333=DIRECTION('center_axis',(0.,0.,1.));
#9334=DIRECTION('ref_axis',(1.,0.,0.));
#18505=CARTESIAN_POINT('',(0.,0.,0.));
#18506=CARTESIAN_POINT('Origin',(0.,0.,0.12));
#18507=CARTESIAN_POINT('',(-0.12639138516214,8.91322620741042E-5,0.00934196736194174));
#18508=CARTESIAN_POINT('',(-0.12645,1.54856587752183E-17,-5.55111512312578E-17));
#18509=CARTESIAN_POINT('',(-0.12645,1.54856587752183E-17,0.12));
#18510=CARTESIAN_POINT('',(-0.0488748409397564,0.116622692573588,0.));
#18511=CARTESIAN_POINT('Origin',(0.,0.,0.));
#18512=CARTESIAN_POINT('Ctrl Pts',(-0.0489111879062984,0.116810626195002,
1.20007714660797E-17));
#18513=CARTESIAN_POINT('Ctrl Pts',(-0.0838963038512042,0.101957324585112,
0.00240024091002088));
#18514=CARTESIAN_POINT('Ctrl Pts',(-0.11198221847721,0.0702793053867637,
0.00480048182004174));
#18515=CARTESIAN_POINT('Ctrl Pts',(-0.122072221370749,0.0336561163696377,
0.00720072273006261));
#18516=CARTESIAN_POINT('Ctrl Pts',(-0.125072637487486,0.022765653033531,
0.00791447094068899));
#18517=CARTESIAN_POINT('Ctrl Pts',(-0.126481745582665,0.0114379076904012,
0.00862821915131536));
#18518=CARTESIAN_POINT('Ctrl Pts',(-0.12639138516214,8.91322620741042E-5,
0.00934196736194174));
#18519=CARTESIAN_POINT('Origin',(0.,0.,0.12));
#18520=CARTESIAN_POINT('',(-0.126396145829628,-9.95859796292312E-5,0.0593419673619417));
#18521=CARTESIAN_POINT('',(-0.126575671592806,-7.20628672610732E-5,0.0456580326380584));
#18522=CARTESIAN_POINT('',(-0.12645,1.54856587752183E-17,0.12));
#18523=CARTESIAN_POINT('',(-0.10808967569503,-0.0656218295092665,0.));
#18524=CARTESIAN_POINT('Ctrl Pts',(-0.126575671592806,-7.20628672610732E-5,
0.0456580326380584));
#18525=CARTESIAN_POINT('Ctrl Pts',(-0.126327459688109,0.0361497101693465,
0.0433719816070355));
#18526=CARTESIAN_POINT('Ctrl Pts',(-0.109912066394173,0.0725710138228805,
0.0410859305760125));
#18527=CARTESIAN_POINT('Ctrl Pts',(-0.0824515099939393,0.0961223418729112,
0.0387998795449896));
#18528=CARTESIAN_POINT('Ctrl Pts',(-0.05137998778939,0.122770586059505,
0.036213220908657));
#18529=CARTESIAN_POINT('Ctrl Pts',(-0.00616751748104999,0.132941603485868,
0.0336265622723243));
#18530=CARTESIAN_POINT('Ctrl Pts',(0.0333172074018229,0.122176268745047,
0.0310399036359917));
#18531=CARTESIAN_POINT('Ctrl Pts',(0.0728019322846963,0.111410934004226,
0.028453244999659));
#18532=CARTESIAN_POINT('Ctrl Pts',(0.106558911742102,0.0797092470962188,
0.0258665863633264));
#18533=CARTESIAN_POINT('Ctrl Pts',(0.11981357554495,0.0409763259700822,
0.0232799277269937));
#18534=CARTESIAN_POINT('Ctrl Pts',(0.133068239347797,0.00224340484394604,
0.0206932690906611));
#18535=CARTESIAN_POINT('Ctrl Pts',(0.125820587496086,-0.0435207505003201,
0.0181066104543285));
#18536=CARTESIAN_POINT('Ctrl Pts',(0.101166903546451,-0.0762076816581678,
0.0155199518179958));
#18537=CARTESIAN_POINT('Ctrl Pts',(0.0765132195968157,-0.108894612816016,
0.0129332931816632));
#18538=CARTESIAN_POINT('Ctrl Pts',(0.0344535035492562,-0.128504319787445,
0.0103466345453306));
#18539=CARTESIAN_POINT('Ctrl Pts',(-0.00636464094143544,-0.126469737202777,
0.00775997590899791));
#18540=CARTESIAN_POINT('Ctrl Pts',(-0.0471827854321269,-0.124435154618108,
0.00517331727266527));
#18541=CARTESIAN_POINT('Ctrl Pts',(-0.0867593583659505,-0.100756282477341,
0.00258665863633259));
#18542=CARTESIAN_POINT('Ctrl Pts',(-0.108089675695031,-0.0656218295092657,
-5.55111512312578E-17));
#18543=CARTESIAN_POINT('Origin',(0.,0.,0.));
#18544=CARTESIAN_POINT('Ctrl Pts',(-0.12639138516214,8.91322620741042E-5,
0.00934196736194174));
#18545=CARTESIAN_POINT('Ctrl Pts',(-0.126154274972366,-0.0296906128949183,
0.011214877787648));
#18546=CARTESIAN_POINT('Ctrl Pts',(-0.115592373032178,-0.0596151635265703,
0.0130877882133543));
#18547=CARTESIAN_POINT('Ctrl Pts',(-0.0963650578556872,-0.0821635787359664,
0.0149606986390606));
#18548=CARTESIAN_POINT('Ctrl Pts',(-0.0698103971670931,-0.113304978845907,
0.0175473572753932));
#18549=CARTESIAN_POINT('Ctrl Pts',(-0.0267272342632827,-0.130377059081323,
0.0201340159117258));
#18550=CARTESIAN_POINT('Ctrl Pts',(0.0139574509341311,-0.125868770046104,
0.0227206745480584));
#18551=CARTESIAN_POINT('Ctrl Pts',(0.0546421361315456,-0.121360481010885,
0.0253073331843911));
#18552=CARTESIAN_POINT('Ctrl Pts',(0.0929283436225635,-0.0952718227050311,
0.0278939918207237));
#18553=CARTESIAN_POINT('Ctrl Pts',(0.112018291148455,-0.0590635258734944,
0.0304806504570564));
#18554=CARTESIAN_POINT('Ctrl Pts',(0.131108238674346,-0.0228552290419586,
0.033067309093389));
#18555=CARTESIAN_POINT('Ctrl Pts',(0.131001926235112,0.0234727063152593,
0.0356539677297216));
#18556=CARTESIAN_POINT('Ctrl Pts',(0.111741771403992,0.0595891814911641,
0.0382406263660542));
#18557=CARTESIAN_POINT('Ctrl Pts',(0.0924816165728724,0.0957056566670696,
0.0408272850023869));
#18558=CARTESIAN_POINT('Ctrl Pts',(0.0540676193498672,0.121610671661662,
0.0434139436387195));
#18559=CARTESIAN_POINT('Ctrl Pts',(0.0133639835211523,0.125930636937597,
0.0460006022750522));
#18560=CARTESIAN_POINT('Ctrl Pts',(-0.0273396523075625,0.130250602213533,
0.0485872609113848));
#18561=CARTESIAN_POINT('Ctrl Pts',(-0.0703329267419868,0.112985517770812,
0.0511739195477175));
#18562=CARTESIAN_POINT('Ctrl Pts',(-0.0967449447385466,0.0817152626609385,
0.0537605781840501));
#18563=CARTESIAN_POINT('Ctrl Pts',(-0.115741878896724,0.0592240248649833,
0.0556210412433473));
#18564=CARTESIAN_POINT('Ctrl Pts',(-0.126160906676814,0.0294875554882879,
0.0574815043026445));
#18565=CARTESIAN_POINT('Ctrl Pts',(-0.126396145829628,-9.95859796292312E-5,
0.0593419673619417));
#18566=CARTESIAN_POINT('Origin',(0.,0.,0.12));
#18567=CARTESIAN_POINT('',(-0.126529791093031,9.025049583615E-5,0.109341967361942));
#18568=CARTESIAN_POINT('',(-0.126349242904067,8.85860673823967E-5,0.0956580326380584));
#18569=CARTESIAN_POINT('',(-0.12645,1.54856587752183E-17,0.12));
#18570=CARTESIAN_POINT('Ctrl Pts',(-0.126349242904067,8.85860673823967E-5,
0.0956580326380584));
#18571=CARTESIAN_POINT('Ctrl Pts',(-0.126441591528965,0.0135570965972842,
0.0948119253946973));
#18572=CARTESIAN_POINT('Ctrl Pts',(-0.124448136217638,0.0269990101701626,
0.0939658181513361));
#18573=CARTESIAN_POINT('Ctrl Pts',(-0.120249444863787,0.0397126388809939,
0.093119710907975));
#18574=CARTESIAN_POINT('Ctrl Pts',(-0.107413505522824,0.0785798365820317,
0.0905330522716423));
#18575=CARTESIAN_POINT('Ctrl Pts',(-0.0739673525896496,0.110640458354997,
0.0879463936353097));
#18576=CARTESIAN_POINT('Ctrl Pts',(-0.0345920580258737,0.121821308595361,
0.085359734998977));
#18577=CARTESIAN_POINT('Ctrl Pts',(0.00478323653790218,0.133002158835724,
0.0827730763626444));
#18578=CARTESIAN_POINT('Ctrl Pts',(0.0500876727322792,0.123303237543486,
0.0801864177263117));
#18579=CARTESIAN_POINT('Ctrl Pts',(0.0814342209129887,0.0969820390626645,
0.077599759089979));
#18580=CARTESIAN_POINT('Ctrl Pts',(0.112780769093698,0.0706608405818426,
0.0750131004536464));
#18581=CARTESIAN_POINT('Ctrl Pts',(0.13016942926074,0.0277173649124373,
0.0724264418173139));
#18582=CARTESIAN_POINT('Ctrl Pts',(0.12596827751407,-0.0129984006283456,
0.0698397831809812));
#18583=CARTESIAN_POINT('Ctrl Pts',(0.121767125767399,-0.0537141661691284,
0.0672531245446486));
#18584=CARTESIAN_POINT('Ctrl Pts',(0.0959761621070158,-0.0922022215812886,
0.0646664659083159));
#18585=CARTESIAN_POINT('Ctrl Pts',(0.059914723710966,-0.111567668284471,
0.0620798072719833));
#18586=CARTESIAN_POINT('Ctrl Pts',(0.0238532853149157,-0.130933114987654,
0.0594931486356506));
#18587=CARTESIAN_POINT('Ctrl Pts',(-0.0224786278168013,-0.131175952981858,
0.056906489999318));
#18588=CARTESIAN_POINT('Ctrl Pts',(-0.0587401909579078,-0.112190380850839,
0.0543198313629853));
#18589=CARTESIAN_POINT('Ctrl Pts',(-0.0950017540990138,-0.0932048087198191,
0.0517331727266527));
#18590=CARTESIAN_POINT('Ctrl Pts',(-0.12119296724951,-0.0549908264635757,
0.0491465140903201));
#18591=CARTESIAN_POINT('Ctrl Pts',(-0.125823286774378,-0.0143210998620416,
0.0465598554539874));
#18592=CARTESIAN_POINT('Ctrl Pts',(-0.126361397696569,-0.0095946821776348,
0.0462592478486778));
#18593=CARTESIAN_POINT('Ctrl Pts',(-0.12660831057823,-0.00483509759607578,
0.0459586402433681));
#18594=CARTESIAN_POINT('Ctrl Pts',(-0.126575671592806,-7.20628672610732E-5,
0.0456580326380584));
#18595=CARTESIAN_POINT('Ctrl Pts',(-0.126396145829628,-9.95859796292312E-5,
0.0593419673619417));
#18596=CARTESIAN_POINT('Ctrl Pts',(-0.12648796685852,-0.0116483513064931,
0.0600681629389771));
#18597=CARTESIAN_POINT('Ctrl Pts',(-0.125028206814926,-0.0231743653405588,
0.0607943585160125));
#18598=CARTESIAN_POINT('Ctrl Pts',(-0.121921363946098,-0.034237873926493,
0.0615205540930479));
#18599=CARTESIAN_POINT('Ctrl Pts',(-0.110855003598394,-0.0736453296270277,
0.0641072127293806));
#18600=CARTESIAN_POINT('Ctrl Pts',(-0.0788915213442898,-0.107184815251071,
0.0666938713657133));
#18601=CARTESIAN_POINT('Ctrl Pts',(-0.0400617348236378,-0.120133683626334,
0.069280530002046));
#18602=CARTESIAN_POINT('Ctrl Pts',(-0.00123194830298627,-0.133082552001597,
0.0718671886383786));
#18603=CARTESIAN_POINT('Ctrl Pts',(0.0444641424842127,-0.125440803128081,
0.0744538472747112));
#18604=CARTESIAN_POINT('Ctrl Pts',(0.0769682295152699,-0.100563001286921,
0.0770405059110438));
#18605=CARTESIAN_POINT('Ctrl Pts',(0.109472316546327,-0.0756851994457607,
0.0796271645473764));
#18606=CARTESIAN_POINT('Ctrl Pts',(0.128784399821243,-0.0335713446369571,
0.0822138231837091));
#18607=CARTESIAN_POINT('Ctrl Pts',(0.126427276285523,0.00729262199647547,
0.0848004818200417));
#18608=CARTESIAN_POINT('Ctrl Pts',(0.124070152749803,0.0481565886299079,
0.0873871404563744));
#18609=CARTESIAN_POINT('Ctrl Pts',(0.100043822403448,0.0877706670879697,
0.0899737990927071));
#18610=CARTESIAN_POINT('Ctrl Pts',(0.0648947831756147,0.108746049780439,
0.0925604577290397));
#18611=CARTESIAN_POINT('Ctrl Pts',(0.0297457439477817,0.129721432472907,
0.0951471163653723));
#18612=CARTESIAN_POINT('Ctrl Pts',(-0.0165260041615291,0.132058119399784,
0.0977337750017049));
#18613=CARTESIAN_POINT('Ctrl Pts',(-0.0536093211433369,0.114730442741844,
0.100320433638038));
#18614=CARTESIAN_POINT('Ctrl Pts',(-0.0906926381251451,0.0974027660839045,
0.10290709227437));
#18615=CARTESIAN_POINT('Ctrl Pts',(-0.11858752397945,0.0604107258411485,
0.105493750910703));
#18616=CARTESIAN_POINT('Ctrl Pts',(-0.12504939731921,0.0199921027543164,
0.108080409547035));
#18617=CARTESIAN_POINT('Ctrl Pts',(-0.126099919499473,0.0134211506765118,
0.108500928818671));
#18618=CARTESIAN_POINT('Ctrl Pts',(-0.126583971845017,0.00675963476331471,
0.108921448090306));
#18619=CARTESIAN_POINT('Ctrl Pts',(-0.126529791093031,9.025049583615E-5,
0.109341967361942));
#18620=CARTESIAN_POINT('Origin',(0.,0.,0.12));
#18621=CARTESIAN_POINT('',(-0.126296536029262,-6.10717992316628E-5,0.159341967361942));
#18622=CARTESIAN_POINT('',(-0.126453631260982,-0.000102348163238207,0.145658032638058));
#18623=CARTESIAN_POINT('',(-0.12645,1.54856587752183E-17,0.12));
#18624=CARTESIAN_POINT('Ctrl Pts',(-0.126453631260982,-0.000102348163238207,
0.145658032638058));
#18625=CARTESIAN_POINT('Ctrl Pts',(-0.126183364177612,0.031552920325249,
0.143665210546026));
#18626=CARTESIAN_POINT('Ctrl Pts',(-0.114073771100105,0.0633928690595716,
0.141672388453994));
#18627=CARTESIAN_POINT('Ctrl Pts',(-0.0925489356314354,0.0864391430514358,
0.139679566361962));
#18628=CARTESIAN_POINT('Ctrl Pts',(-0.0646099631645552,0.116352924063146,
0.13709290772563));
#18629=CARTESIAN_POINT('Ctrl Pts',(-0.0208084524006029,0.131451366650306,
0.134506249089297));
#18630=CARTESIAN_POINT('Ctrl Pts',(0.0196287675426836,0.125106932552633,
0.131919590452964));
#18631=CARTESIAN_POINT('Ctrl Pts',(0.0600659874859703,0.11876249845496,
0.129332931816632));
#18632=CARTESIAN_POINT('Ctrl Pts',(0.097138916608591,0.0909751876724545,
0.126746273180299));
#18633=CARTESIAN_POINT('Ctrl Pts',(0.114574233156503,0.0539423598350403,
0.124159614543967));
#18634=CARTESIAN_POINT('Ctrl Pts',(0.132009549704415,0.0169095319976262,
0.121572955907634));
#18635=CARTESIAN_POINT('Ctrl Pts',(0.129807253677619,-0.0293688128946969,
0.118986297271301));
#18636=CARTESIAN_POINT('Ctrl Pts',(0.108934072954415,-0.0645786240759305,
0.116399638634969));
#18637=CARTESIAN_POINT('Ctrl Pts',(0.0880608922312115,-0.099788435257164,
0.113812979998636));
#18638=CARTESIAN_POINT('Ctrl Pts',(0.0485168268116012,-0.123929712727308,
0.111226321362303));
#18639=CARTESIAN_POINT('Ctrl Pts',(0.00765986125275547,-0.126405537442516,
0.108639662725971));
#18640=CARTESIAN_POINT('Ctrl Pts',(-0.0331971043060904,-0.128881362157723,
0.106053004089638));
#18641=CARTESIAN_POINT('Ctrl Pts',(-0.0753669700041717,-0.109691734117994,
0.103466345453305));
#18642=CARTESIAN_POINT('Ctrl Pts',(-0.100339039978837,-0.0772600332835736,
0.100879686816973));
#18643=CARTESIAN_POINT('Ctrl Pts',(-0.117142637704978,-0.0554368822612891,
0.0991391354240014));
#18644=CARTESIAN_POINT('Ctrl Pts',(-0.126159269908366,-0.0276178718881664,
0.0973985840310299));
#18645=CARTESIAN_POINT('Ctrl Pts',(-0.126349242904067,8.85860673823967E-5,
0.0956580326380584));
#18646=CARTESIAN_POINT('Ctrl Pts',(-0.126529791093031,9.025049583615E-5,
0.109341967361942));
#18647=CARTESIAN_POINT('Ctrl Pts',(-0.126250700293628,-0.0342644551610371,
0.111508106726639));
#18648=CARTESIAN_POINT('Ctrl Pts',(-0.111690189779818,-0.0688279388928191,
0.113674246091336));
#18649=CARTESIAN_POINT('Ctrl Pts',(-0.0867076257192948,-0.092297473337895,
0.115840385456033));
#18650=CARTESIAN_POINT('Ctrl Pts',(-0.0568751199544048,-0.120323220412367,
0.118427044092366));
#18651=CARTESIAN_POINT('Ctrl Pts',(-0.0121812475994092,-0.132529508630403,
0.121013702728699));
#18652=CARTESIAN_POINT('Ctrl Pts',(0.0277554439013372,-0.123558363290506,
0.123600361365031));
#18653=CARTESIAN_POINT('Ctrl Pts',(0.0676921354020838,-0.114587217950609,
0.126187020001364));
#18654=CARTESIAN_POINT('Ctrl Pts',(0.102871646048582,-0.0844386390527785,
0.128773678637697));
#18655=CARTESIAN_POINT('Ctrl Pts',(0.117851793294146,-0.0463464242807743,
0.131360337274029));
#18656=CARTESIAN_POINT('Ctrl Pts',(0.13283194053971,-0.00825420950877041,
0.133946995910362));
#18657=CARTESIAN_POINT('Ctrl Pts',(0.127612724384341,0.0377816411374068,
0.136533654546694));
#18658=CARTESIAN_POINT('Ctrl Pts',(0.104485135941302,0.0715534408109559,
0.139120313183027));
#18659=CARTESIAN_POINT('Ctrl Pts',(0.0813575474982633,0.105325240484505,
0.14170697181936));
#18660=CARTESIAN_POINT('Ctrl Pts',(0.0403215867675544,0.126832989185426,
0.144293630455692));
#18661=CARTESIAN_POINT('Ctrl Pts',(-0.000609841963000384,0.126635909896556,
0.146880289092025));
#18662=CARTESIAN_POINT('Ctrl Pts',(-0.0415412706935549,0.126438830607686,
0.149466947728358));
#18663=CARTESIAN_POINT('Ctrl Pts',(-0.0823681674239554,0.104536923329025,
0.15205360636469));
#18664=CARTESIAN_POINT('Ctrl Pts',(-0.10516942503222,0.0705438627883669,
0.154640265001023));
#18665=CARTESIAN_POINT('Ctrl Pts',(-0.118984510025511,0.0499477610899654,
0.156207499121329));
#18666=CARTESIAN_POINT('Ctrl Pts',(-0.126182304652747,0.0249129445447297,
0.157774733241635));
#18667=CARTESIAN_POINT('Ctrl Pts',(-0.126296536029262,-6.10717992316628E-5,
0.159341967361942));
#18668=CARTESIAN_POINT('Origin',(0.,0.,0.12));
#18669=CARTESIAN_POINT('',(-0.126625441102054,2.7778768752873E-5,0.209341967361942));
#18670=CARTESIAN_POINT('',(-0.126471935391749,0.000101176582396995,0.195658032638058));
#18671=CARTESIAN_POINT('',(-0.12645,1.54856587752183E-17,0.12));
#18672=CARTESIAN_POINT('',(0.0958116152722397,0.0825211298936481,0.24));
#18673=CARTESIAN_POINT('Ctrl Pts',(-0.126625441102054,2.7778768752873E-5,
0.209341967361942));
#18674=CARTESIAN_POINT('Ctrl Pts',(-0.126482885932031,-0.0388928622545336,
0.21180133566563));
#18675=CARTESIAN_POINT('Ctrl Pts',(-0.107125339127294,-0.077921419747323,
0.214260703969318));
#18676=CARTESIAN_POINT('Ctrl Pts',(-0.0759952538809665,-0.101287130411732,
0.216720072273006));
#18677=CARTESIAN_POINT('Ctrl Pts',(-0.0432539585932993,-0.12586218783339,
0.219306730909339));
#18678=CARTESIAN_POINT('Ctrl Pts',(0.0025100419330305,-0.133111106253138,
0.221893389545672));
#18679=CARTESIAN_POINT('Ctrl Pts',(0.0412155518054008,-0.119764891216682,
0.224480048182004));
#18680=CARTESIAN_POINT('Ctrl Pts',(0.0799210616777711,-0.106418676180227,
0.227066706818337));
#18681=CARTESIAN_POINT('Ctrl Pts',(0.111568080896182,-0.072477327687567,
0.229653365454669));
#18682=CARTESIAN_POINT('Ctrl Pts',(0.122246574267713,-0.0330282462555153,
0.232240024091002));
#18683=CARTESIAN_POINT('Ctrl Pts',(0.132925067639245,0.00642083517653631,
0.234826682727335));
#18684=CARTESIAN_POINT('Ctrl Pts',(0.122635035163896,0.0513776495479799,
0.237413341363667));
#18685=CARTESIAN_POINT('Ctrl Pts',(0.0958116152722397,0.0825211298936481,
0.24));
#18686=CARTESIAN_POINT('',(-0.0959791030802601,0.0826138105732953,0.24));
#18687=CARTESIAN_POINT('Origin',(0.,0.,0.24));
#18688=CARTESIAN_POINT('Ctrl Pts',(-0.0959791030802601,0.0826138105732953,
0.24));
#18689=CARTESIAN_POINT('Ctrl Pts',(-0.0710417758635208,0.111296717646776,
0.237599759089979));
#18690=CARTESIAN_POINT('Ctrl Pts',(-0.0322351762885183,0.128218895525122,
0.235199518179958));
#18691=CARTESIAN_POINT('Ctrl Pts',(0.00571352152256588,0.126497857083363,
0.232799277269937));
#18692=CARTESIAN_POINT('Ctrl Pts',(0.0466095526337785,0.124643152028446,
0.230212618633605));
#18693=CARTESIAN_POINT('Ctrl Pts',(0.0865092470399708,0.101136876245298,
0.227625959997272));
#18694=CARTESIAN_POINT('Ctrl Pts',(0.107920636628548,0.0662586835305903,
0.225039301360939));
#18695=CARTESIAN_POINT('Ctrl Pts',(0.129332026217125,0.0313804908158828,
0.222452642724607));
#18696=CARTESIAN_POINT('Ctrl Pts',(0.132255110988087,-0.014869618830384,
0.219865984088274));
#18697=CARTESIAN_POINT('Ctrl Pts',(0.115395215428634,-0.0521699181865619,
0.217279325451942));
#18698=CARTESIAN_POINT('Ctrl Pts',(0.0985353198691812,-0.0894702175427398,
0.214692666815609));
#18699=CARTESIAN_POINT('Ctrl Pts',(0.0618924439793129,-0.117820706608829,
0.212106008179276));
#18700=CARTESIAN_POINT('Ctrl Pts',(0.0215571925812854,-0.12478734248304,
0.209519349542944));
#18701=CARTESIAN_POINT('Ctrl Pts',(-0.0187780588167422,-0.13175397835725,
0.206932690906611));
#18702=CARTESIAN_POINT('Ctrl Pts',(-0.0628056857229291,-0.117336761039583,
0.204346032270278));
#18703=CARTESIAN_POINT('Ctrl Pts',(-0.0912027768750998,-0.0878586653637446,
0.201759373633946));
#18704=CARTESIAN_POINT('Ctrl Pts',(-0.113530209130371,-0.0646812849521466,
0.199725593301983));
#18705=CARTESIAN_POINT('Ctrl Pts',(-0.126194825294183,-0.0321932513395888,
0.197691812970021));
#18706=CARTESIAN_POINT('Ctrl Pts',(-0.126471935391749,0.000101176582396995,
0.195658032638058));
#18707=CARTESIAN_POINT('Origin',(0.,0.,0.350421172358873));
#18708=CARTESIAN_POINT('',(-0.154453350152392,-8.79343647196378E-5,0.0295788276411275));
#18709=CARTESIAN_POINT('',(-0.15422847552802,0.000108763211052777,0.025421172358873));
#18710=CARTESIAN_POINT('',(-0.1543,-1.01731279388251E-15,0.350421172358873));
#18711=CARTESIAN_POINT('',(0.15408394018464,-0.00816268198427004,0.));
#18712=CARTESIAN_POINT('Ctrl Pts',(-0.15422847552802,0.000108763211052763,
0.025421172358873));
#18713=CARTESIAN_POINT('Ctrl Pts',(-0.154338737393477,0.0139570514561378,
0.0247074241482466));
#18714=CARTESIAN_POINT('Ctrl Pts',(-0.146387882101843,0.0778735560251454,
0.0214070173012875));
#18715=CARTESIAN_POINT('Ctrl Pts',(-0.0581466660421577,0.171532975008042,
0.0155199518179959));
#18716=CARTESIAN_POINT('Ctrl Pts',(0.109502662757235,0.144085240745689,
0.00775997590899784));
#18717=CARTESIAN_POINT('Ctrl Pts',(0.156737212705124,0.0419221657566679,
0.00258665863633264));
#18718=CARTESIAN_POINT('Ctrl Pts',(0.15408394018464,-0.00816268198427004,
0.));
#18719=CARTESIAN_POINT('',(0.129620323775263,-0.0841289546921688,3.62607491890453E-17));
#18720=CARTESIAN_POINT('Origin',(0.,0.,0.));
#18721=CARTESIAN_POINT('Ctrl Pts',(-0.154453350152392,-8.7934364719636E-5,
0.0295788276411275));
#18722=CARTESIAN_POINT('Ctrl Pts',(-0.154150470777978,0.0441115087317509,
0.0272927766101045));
#18723=CARTESIAN_POINT('Ctrl Pts',(-0.111454882743928,0.138841433785012,
0.0224200669427489));
#18724=CARTESIAN_POINT('Ctrl Pts',(0.0476444145610997,0.174632482457551,
0.0149606986390605));
#18725=CARTESIAN_POINT('Ctrl Pts',(0.168251138196633,0.0613688951001999,
0.0073871404563744));
#18726=CARTESIAN_POINT('Ctrl Pts',(0.154676764047789,-0.0451013867871701,
0.00240024091002087));
#18727=CARTESIAN_POINT('Ctrl Pts',(0.129620323775263,-0.0841289546921688,
1.57209315010398E-17));
#18728=CARTESIAN_POINT('Origin',(0.,0.,0.350421172358873));
#18729=CARTESIAN_POINT('',(-0.154177051641736,0.000108096719625833,0.0795788276411275));
#18730=CARTESIAN_POINT('',(-0.154234284709463,-0.000121519309271207,0.075421172358873));
#18731=CARTESIAN_POINT('',(-0.1543,-1.01731279388251E-15,0.350421172358873));
#18732=CARTESIAN_POINT('Ctrl Pts',(-0.154234284709463,-0.000121519309271208,
0.0754211723588731));
#18733=CARTESIAN_POINT('Ctrl Pts',(-0.153947235272697,0.0359820467524117,
0.0735607092995758));
#18734=CARTESIAN_POINT('Ctrl Pts',(-0.123557126730793,0.122717061869437,
0.0691135876039459));
#18735=CARTESIAN_POINT('Ctrl Pts',(0.0191012565771036,0.180005302104073,
0.0620798072719832));
#18736=CARTESIAN_POINT('Ctrl Pts',(0.159724738700703,0.0851738948996701,
0.0543198313629854));
#18737=CARTESIAN_POINT('Ctrl Pts',(0.160113920417758,-0.0844204212478698,
0.0465598554539874));
#18738=CARTESIAN_POINT('Ctrl Pts',(0.0199582426985643,-0.179924098035372,
0.0387998795449896));
#18739=CARTESIAN_POINT('Ctrl Pts',(-0.123251388539896,-0.123176028715441,
0.0317536518466181));
#18740=CARTESIAN_POINT('Ctrl Pts',(-0.153939142967466,-0.0362298265692857,
0.0272940827845792));
#18741=CARTESIAN_POINT('Ctrl Pts',(-0.15422847552802,0.000108763211052763,
0.025421172358873));
#18742=CARTESIAN_POINT('Ctrl Pts',(-0.154177051641736,0.000108096719625859,
0.0795788276411275));
#18743=CARTESIAN_POINT('Ctrl Pts',(-0.154289739603949,0.0165429814548096,
0.0787327203977663));
#18744=CARTESIAN_POINT('Ctrl Pts',(-0.144420757340354,0.0830897487115299,
0.0752999545180725));
#18745=CARTESIAN_POINT('Ctrl Pts',(-0.0494457976037486,0.174130301808973,
0.0692805300020459));
#18746=CARTESIAN_POINT('Ctrl Pts',(0.11640175885633,0.13862511662766,0.061520554093048));
#18747=CARTESIAN_POINT('Ctrl Pts',(0.18005704388064,-0.0185795878987759,
0.0537605781840501));
#18748=CARTESIAN_POINT('Ctrl Pts',(0.0856431484406112,-0.159474177462153,
0.0460006022750521));
#18749=CARTESIAN_POINT('Ctrl Pts',(-0.0839657292871194,-0.160363143120653,
0.0382406263660544));
#18750=CARTESIAN_POINT('Ctrl Pts',(-0.151599316432495,-0.0616831513139142,
0.0327667014880793));
#18751=CARTESIAN_POINT('Ctrl Pts',(-0.154493177716258,-0.00590000442131094,
0.0298794352464371));
#18752=CARTESIAN_POINT('Ctrl Pts',(-0.154453350152392,-8.7934364719636E-5,
0.0295788276411275));
#18753=CARTESIAN_POINT('Origin',(0.,0.,0.350421172358873));
#18754=CARTESIAN_POINT('',(-0.154304431028624,-0.000124889850439479,0.129578827641127));
#18755=CARTESIAN_POINT('',(-0.154397364694779,0.000110127730384366,0.125421172358873));
#18756=CARTESIAN_POINT('',(-0.1543,-1.01731279388251E-15,0.350421172358873));
#18757=CARTESIAN_POINT('Ctrl Pts',(-0.154397364694779,0.000110127730384357,
0.125421172358873));
#18758=CARTESIAN_POINT('Ctrl Pts',(-0.154463478494948,0.00824841157753406,
0.125000653087238));
#18759=CARTESIAN_POINT('Ctrl Pts',(-0.150239588102603,0.0663774823757793,
0.121993475179269));
#18760=CARTESIAN_POINT('Ctrl Pts',(-0.0766286530280003,0.163994611436961,
0.116399638634969));
#18761=CARTESIAN_POINT('Ctrl Pts',(0.0927599764682439,0.155440618724813,
0.108639662725971));
#18762=CARTESIAN_POINT('Ctrl Pts',(0.180714016146597,0.0104239566588842,
0.100879686816973));
#18763=CARTESIAN_POINT('Ctrl Pts',(0.11001758793024,-0.143743725357685,
0.093119710907975));
#18764=CARTESIAN_POINT('Ctrl Pts',(-0.0572637123892103,-0.171718146500831,
0.0853597349989769));
#18765=CARTESIAN_POINT('Ctrl Pts',(-0.146220320052713,-0.0783754111826042,
0.0794602221492764));
#18766=CARTESIAN_POINT('Ctrl Pts',(-0.154346328875204,-0.0142138442593302,
0.0761473679359084));
#18767=CARTESIAN_POINT('Ctrl Pts',(-0.154234284709463,-0.000121519309271208,
0.0754211723588731));
#18768=CARTESIAN_POINT('Ctrl Pts',(-0.154304431028624,-0.000124889850439474,
0.129578827641127));
#18769=CARTESIAN_POINT('Ctrl Pts',(-0.153974638929265,0.0385022981904757,
0.127586005549095));
#18770=CARTESIAN_POINT('Ctrl Pts',(-0.120018027207353,0.127784966030512,
0.123006524820731));
#18771=CARTESIAN_POINT('Ctrl Pts',(0.0280571680938306,0.178826694862324,
0.115840385456033));
#18772=CARTESIAN_POINT('Ctrl Pts',(0.163771354656592,0.0771047007047774,
0.108080409547035));
#18773=CARTESIAN_POINT('Ctrl Pts',(0.155709331479018,-0.0923080778690166,
0.100320433638038));
#18774=CARTESIAN_POINT('Ctrl Pts',(0.0109489686262093,-0.180682908560435,
0.0925604577290397));
#18775=CARTESIAN_POINT('Ctrl Pts',(-0.126591758993125,-0.118094248159534,
0.0856465890634029));
#18776=CARTESIAN_POINT('Ctrl Pts',(-0.153945238013925,-0.0337005743957639,
0.0813193790340989));
#18777=CARTESIAN_POINT('Ctrl Pts',(-0.154177051641736,0.000108096719625859,
0.0795788276411275));
#18778=CARTESIAN_POINT('Origin',(0.,0.,0.350421172358873));
#18779=CARTESIAN_POINT('',(-0.154326766555531,0.000123460234585843,0.179578827641127));
#18780=CARTESIAN_POINT('',(-0.154112736333057,-7.45225671948511E-5,0.175421172358873));
#18781=CARTESIAN_POINT('',(-0.1543,-1.01731279388251E-15,0.350421172358873));
#18782=CARTESIAN_POINT('Ctrl Pts',(-0.154112736333057,-7.45225671948471E-5,
0.175421172358873));
#18783=CARTESIAN_POINT('Ctrl Pts',(-0.153973346049181,0.0303998999070902,
0.173853938238567));
#18784=CARTESIAN_POINT('Ctrl Pts',(-0.130694151755309,0.111367805862998,
0.169700045481928));
#18785=CARTESIAN_POINT('Ctrl Pts',(-0.000871711368246156,0.181012066871201,
0.162959494088956));
#18786=CARTESIAN_POINT('Ctrl Pts',(0.149350085565286,0.102277888352765,
0.155199518179958));
#18787=CARTESIAN_POINT('Ctrl Pts',(0.168456255263351,-0.0662471829332422,
0.14743954227096));
#18788=CARTESIAN_POINT('Ctrl Pts',(0.0396733728729688,-0.17661315503135,
0.139679566361963));
#18789=CARTESIAN_POINT('Ctrl Pts',(-0.115072782317819,-0.134350623919955,
0.1323401097246));
#18790=CARTESIAN_POINT('Ctrl Pts',(-0.154056805498669,-0.041811035439686,
0.12758731172357));
#18791=CARTESIAN_POINT('Ctrl Pts',(-0.154397364694779,0.000110127730384357,
0.125421172358873));
#18792=CARTESIAN_POINT('Ctrl Pts',(-0.154326766555531,0.000123460234585825,
0.179578827641127));
#18793=CARTESIAN_POINT('Ctrl Pts',(-0.154418689716183,0.0108361910665024,
0.179025949336757));
#18794=CARTESIAN_POINT('Ctrl Pts',(-0.148597337680631,0.071569631208062,
0.175886412396054));
#18795=CARTESIAN_POINT('Ctrl Pts',(-0.0683530255288039,0.167611467503216,
0.170160216819019));
#18796=CARTESIAN_POINT('Ctrl Pts',(0.100397202365132,0.150621028353064,
0.162400240910021));
#18797=CARTESIAN_POINT('Ctrl Pts',(0.18100910679194,0.00139719974911195,
0.154640265001023));
#18798=CARTESIAN_POINT('Ctrl Pts',(0.102711092909207,-0.149052183789333,
0.146880289092025));
#18799=CARTESIAN_POINT('Ctrl Pts',(-0.0657574679958034,-0.168648048308422,
0.139120313183027));
#18800=CARTESIAN_POINT('Ctrl Pts',(-0.148058381688037,-0.0731761882111772,
0.133353159366061));
#18801=CARTESIAN_POINT('Ctrl Pts',(-0.154402705029802,-0.0116353181791797,
0.130172664185428));
#18802=CARTESIAN_POINT('Ctrl Pts',(-0.154304431028624,-0.000124889850439474,
0.129578827641127));
#18803=CARTESIAN_POINT('Origin',(0.,0.,0.350421172358873));
#18804=CARTESIAN_POINT('',(-0.154128406284035,-0.000157308197905263,0.229578827641128));
#18805=CARTESIAN_POINT('',(-0.154514081154978,3.38969080117728E-5,0.225421172358873));
#18806=CARTESIAN_POINT('',(-0.1543,-1.01731279388251E-15,0.350421172358873));
#18807=CARTESIAN_POINT('',(-0.0398513841857245,-0.149064942821851,0.24));
#18808=CARTESIAN_POINT('Ctrl Pts',(-0.0398513841857245,-0.149064942821851,
0.24));
#18809=CARTESIAN_POINT('Ctrl Pts',(-0.0883048112969314,-0.136111285829332,
0.237413341363667));
#18810=CARTESIAN_POINT('Ctrl Pts',(-0.143745772087175,-0.0847488633265083,
0.233939617244043));
#18811=CARTESIAN_POINT('Ctrl Pts',(-0.154234229255939,-0.017399338864059,
0.230465893124419));
#18812=CARTESIAN_POINT('Ctrl Pts',(-0.154128406284035,-0.00015730819790527,
0.229578827641128));
#18813=CARTESIAN_POINT('',(0.0399565498027962,-0.149273502906638,0.24));
#18814=CARTESIAN_POINT('Origin',(0.,0.,0.24));
#18815=CARTESIAN_POINT('Ctrl Pts',(0.0399565498027963,-0.149273502906638,
0.24));
#18816=CARTESIAN_POINT('Ctrl Pts',(-0.00490373130458673,-0.161043406468747,
0.237599759089979));
#18817=CARTESIAN_POINT('Ctrl Pts',(-0.107666111297752,-0.141562671532916,
0.23274014987627));
#18818=CARTESIAN_POINT('Ctrl Pts',(-0.154340128899266,-0.0474588267763927,
0.227880540662561));
#18819=CARTESIAN_POINT('Ctrl Pts',(-0.154514081154978,3.3896908011755E-5,
0.225421172358873));
#18820=CARTESIAN_POINT('Origin',(0.,0.,0.350421172358873));
#18821=CARTESIAN_POINT('Ctrl Pts',(-0.154514081154978,3.3896908011755E-5,
0.225421172358873));
#18822=CARTESIAN_POINT('Ctrl Pts',(-0.154523084458981,0.00249199339844659,
0.225293882026228));
#18823=CARTESIAN_POINT('Ctrl Pts',(-0.153375868586475,0.0548933889046004,
0.222579933057251));
#18824=CARTESIAN_POINT('Ctrl Pts',(-0.0942515706791253,0.154556313135293,
0.217279325451942));
#18825=CARTESIAN_POINT('Ctrl Pts',(0.0750450248431312,0.164716481511431,
0.209519349542944));
#18826=CARTESIAN_POINT('Ctrl Pts',(0.178461260043253,0.0303012077178856,
0.201759373633945));
#18827=CARTESIAN_POINT('Ctrl Pts',(0.125203781387627,-0.130731709675357,
0.193999397724948));
#18828=CARTESIAN_POINT('Ctrl Pts',(-0.0379704533096903,-0.17698585337688,
0.18623942181595));
#18829=CARTESIAN_POINT('Ctrl Pts',(-0.141587477595567,-0.0899051669249145,
0.180046680027258));
#18830=CARTESIAN_POINT('Ctrl Pts',(-0.154203404262525,-0.019896942829432,
0.176440596874899));
#18831=CARTESIAN_POINT('Ctrl Pts',(-0.154112736333057,-7.45225671948471E-5,
0.175421172358873));
#18832=CARTESIAN_POINT('Ctrl Pts',(-0.154128406284035,-0.00015730819790527,
0.229578827641128));
#18833=CARTESIAN_POINT('Ctrl Pts',(-0.153925652370292,0.0328779499839183,
0.227879234488086));
#18834=CARTESIAN_POINT('Ctrl Pts',(-0.127638532780061,0.116591914860373,
0.223592982698713));
#18835=CARTESIAN_POINT('Ctrl Pts',(0.00818767200092134,0.180778621679153,
0.216720072273006));
#18836=CARTESIAN_POINT('Ctrl Pts',(0.154249898498561,0.0947283641859207,
0.208960096364008));
#18837=CARTESIAN_POINT('Ctrl Pts',(0.164950538597243,-0.0745810526211722,
0.201200120455011));
#18838=CARTESIAN_POINT('Ctrl Pts',(0.0308106631569891,-0.178364693496558,
0.193440144546012));
#18839=CARTESIAN_POINT('Ctrl Pts',(-0.118879635670858,-0.129347344159377,
0.186233046941385));
#18840=CARTESIAN_POINT('Ctrl Pts',(-0.153988624301243,-0.0392836590090855,
0.18161260797309));
#18841=CARTESIAN_POINT('Ctrl Pts',(-0.154326766555531,0.000123460234585825,
0.179578827641127));
#18842=CARTESIAN_POINT('Ctrl Pts',(0.0958116152722397,0.0825211298936481,
0.24));
#18843=CARTESIAN_POINT('Ctrl Pts',(0.122635035163896,0.0513776495479799,
0.237413341363667));
#18844=CARTESIAN_POINT('Ctrl Pts',(0.143215100114593,-0.0385359791949074,
0.232240024091002));
#18845=CARTESIAN_POINT('Ctrl Pts',(0.0482740424593604,-0.140360024672886,
0.224480048182004));
#18846=CARTESIAN_POINT('Ctrl Pts',(-0.0890179591196291,-0.118613269413641,
0.216720072273006));
#18847=CARTESIAN_POINT('Ctrl Pts',(-0.148173729266643,0.00709031985706173,
0.208960096364008));
#18848=CARTESIAN_POINT('Ctrl Pts',(-0.0772398646297824,0.126660050524678,
0.20120012045501));
#18849=CARTESIAN_POINT('Ctrl Pts',(0.0614999571705377,0.134986384232796,
0.193440144546013));
#18850=CARTESIAN_POINT('Ctrl Pts',(0.146250332679645,0.0248320655601208,
0.185680168637014));
#18851=CARTESIAN_POINT('Ctrl Pts',(0.102605431992647,-0.107135610424167,
0.177920192728017));
#18852=CARTESIAN_POINT('Ctrl Pts',(-0.0311170694815965,-0.145041225920327,
0.170160216819019));
#18853=CARTESIAN_POINT('Ctrl Pts',(-0.137521919612742,-0.0556176253575994,
0.162400240910021));
#18854=CARTESIAN_POINT('Ctrl Pts',(-0.123195064154356,0.0826350160503635,
0.154640265001023));
#18855=CARTESIAN_POINT('Ctrl Pts',(-0.000714373963154436,0.148340737886347,
0.146880289092025));
#18856=CARTESIAN_POINT('Ctrl Pts',(0.122393508228972,0.0838174917835845,
0.139120313183027));
#18857=CARTESIAN_POINT('Ctrl Pts',(0.138051156695079,-0.0542900601549481,
0.131360337274029));
#18858=CARTESIAN_POINT('Ctrl Pts',(0.032512624755586,-0.14473579684844,
0.123600361365031));
#18859=CARTESIAN_POINT('Ctrl Pts',(-0.101568992309399,-0.108116932194331,
0.115840385456033));
#18860=CARTESIAN_POINT('Ctrl Pts',(-0.146482409833755,0.0234186855983926,
0.108080409547036));
#18861=CARTESIAN_POINT('Ctrl Pts',(-0.0627977522708403,0.13439480632666,
0.100320433638038));
#18862=CARTESIAN_POINT('Ctrl Pts',(0.076017492057093,0.127384745546031,
0.0925604577290397));
#18863=CARTESIAN_POINT('Ctrl Pts',(0.148096483096158,0.00854251017184644,
0.0848004818200417));
#18864=CARTESIAN_POINT('Ctrl Pts',(0.0901602332714121,-0.117799054254564,
0.0770405059110438));
#18865=CARTESIAN_POINT('Ctrl Pts',(-0.0469280390901857,-0.140724300875114,
0.069280530002046));
#18866=CARTESIAN_POINT('Ctrl Pts',(-0.142818485852497,-0.0401058440029853,
0.0615205540930479));
#18867=CARTESIAN_POINT('Ctrl Pts',(-0.113326201176411,0.0957204333280909,
0.0537605781840501));
#18868=CARTESIAN_POINT('Ctrl Pts',(0.0156536221268617,0.147515686656254,
0.0460006022750521));
#18869=CARTESIAN_POINT('Ctrl Pts',(0.130895613795878,0.0698006416724775,
0.0382406263660543));
#18870=CARTESIAN_POINT('Ctrl Pts',(0.13121455111358,-0.0691831643991777,
0.0304806504570563));
#18871=CARTESIAN_POINT('Ctrl Pts',(0.0163559286405278,-0.147449139316739,
0.0227206745480584));
#18872=CARTESIAN_POINT('Ctrl Pts',(-0.112893560070904,-0.0962328986104914,
0.0149606986390606));
#18873=CARTESIAN_POINT('Ctrl Pts',(-0.142972035491037,0.0393992613429074,
0.00720072273006258));
#18874=CARTESIAN_POINT('Ctrl Pts',(-0.0476516261894416,0.140572551456688,
-0.000559253178935252));
#18875=CARTESIAN_POINT('Ctrl Pts',(0.0897382482543901,0.118078928660352,
-0.00831922908793326));
#18876=CARTESIAN_POINT('Ctrl Pts',(0.128447313976429,0.0343555272840613,
-0.0134925463605985));
#18877=CARTESIAN_POINT('Ctrl Pts',(0.126272937371016,-0.00668937872268922,
-0.0160792049969311));
#18878=CARTESIAN_POINT('Ctrl Pts',(0.102845629995666,0.0885794229410663,
0.245359734998977));
#18879=CARTESIAN_POINT('Ctrl Pts',(0.13163829265517,0.0551495423644061,
0.242773076362644));
#18880=CARTESIAN_POINT('Ctrl Pts',(0.153729244145676,-0.0413651001137901,
0.237599759089979));
#18881=CARTESIAN_POINT('Ctrl Pts',(0.0518180837997932,-0.150664563191773,
0.229839783180981));
#18882=CARTESIAN_POINT('Ctrl Pts',(-0.0955532172229155,-0.127321268762976,
0.222079807271983));
#18883=CARTESIAN_POINT('Ctrl Pts',(-0.159051911315084,0.00761085605850937,
0.214319831362985));
#18884=CARTESIAN_POINT('Ctrl Pts',(-0.0829104333128967,0.135958804728216,
0.206559855453988));
#18885=CARTESIAN_POINT('Ctrl Pts',(0.0660149797280689,0.144896416659008,
0.19879987954499));
#18886=CARTESIAN_POINT('Ctrl Pts',(0.156987308467515,0.0266551129460425,
0.191039903635992));
#18887=CARTESIAN_POINT('Ctrl Pts',(0.110138215124307,-0.11500097684123,
0.183279927726994));
#18888=CARTESIAN_POINT('Ctrl Pts',(-0.0334015307576278,-0.155689435072511,
0.175519951817996));
#18889=CARTESIAN_POINT('Ctrl Pts',(-0.147618098500879,-0.0597007962188336,
0.167759975908998));
#18890=CARTESIAN_POINT('Ctrl Pts',(-0.13223943620312,0.0887016700559064,
0.16));
#18891=CARTESIAN_POINT('Ctrl Pts',(-0.000766819764851659,0.159231180881298,
0.152240024091002));
#18892=CARTESIAN_POINT('Ctrl Pts',(0.131379034007743,0.0899709573066447,
0.144480048182004));
#18893=CARTESIAN_POINT('Ctrl Pts',(0.14818618955117,-0.0582757677477129,
0.136720072273006));
#18894=CARTESIAN_POINT('Ctrl Pts',(0.0348995407947136,-0.15536158290941,
0.128960096364009));
#18895=CARTESIAN_POINT('Ctrl Pts',(-0.109025685167754,-0.116054342400242,
0.12120012045501));
#18896=CARTESIAN_POINT('Ctrl Pts',(-0.157236423577976,0.0251379696208395,
0.113440144546013));
#18897=CARTESIAN_POINT('Ctrl Pts',(-0.0674080525232269,0.144261408030094,
0.105680168637014));
#18898=CARTESIAN_POINT('Ctrl Pts',(0.0815983201941432,0.136736703272292,
0.0979201927280168));
#18899=CARTESIAN_POINT('Ctrl Pts',(0.158968994112971,0.00916965900085902,
0.0901602168190187));
#18900=CARTESIAN_POINT('Ctrl Pts',(0.0967793514910216,-0.126447277955604,
0.0824002409100209));
#18901=CARTESIAN_POINT('Ctrl Pts',(-0.0503732635231939,-0.151055582750353,
0.0746402650010229));
#18902=CARTESIAN_POINT('Ctrl Pts',(-0.15330351242688,-0.0430502166284845,
0.066880289092025));
#18903=CARTESIAN_POINT('Ctrl Pts',(-0.121646050135849,0.102747753924341,
0.0591203131830272));
#18904=CARTESIAN_POINT('Ctrl Pts',(0.0168028336102756,0.158345558472194,
0.0513603372740292));
#18905=CARTESIAN_POINT('Ctrl Pts',(0.140505322097486,0.074925059414875,
0.0436003613650313));
#18906=CARTESIAN_POINT('Ctrl Pts',(0.140847674214973,-0.0742622500154084,
0.0358403854560334));
#18907=CARTESIAN_POINT('Ctrl Pts',(0.0175566999932067,-0.158274125556283,
0.0280804095470355));
#18908=CARTESIAN_POINT('Ctrl Pts',(-0.121181646661057,-0.103297841872129,
0.0203204336380376));
#18909=CARTESIAN_POINT('Ctrl Pts',(-0.153468334920127,0.0422917601656304,
0.0125604577290396));
#18910=CARTESIAN_POINT('Ctrl Pts',(-0.0511499728070136,0.150892692640473,
0.00480048182004178));
#18911=CARTESIAN_POINT('Ctrl Pts',(0.0963263864220051,0.126747699355464,
-0.00295949408895622));
#18912=CARTESIAN_POINT('Ctrl Pts',(0.137877280219327,0.0368777401082635,
-0.00813281136162143));
#18913=CARTESIAN_POINT('Ctrl Pts',(0.135543271642224,-0.00718047980988283,
-0.0107194699979541));
#18914=CARTESIAN_POINT('Ctrl Pts',(0.109879644719093,0.0946377159884845,
0.250719469997954));
#18915=CARTESIAN_POINT('Ctrl Pts',(0.140641550146443,0.0589214351808321,
0.248132811361621));
#18916=CARTESIAN_POINT('Ctrl Pts',(0.164243388176759,-0.0441942210326729,
0.242959494088956));
#18917=CARTESIAN_POINT('Ctrl Pts',(0.055362125140226,-0.160969101710661,
0.235199518179958));
#18918=CARTESIAN_POINT('Ctrl Pts',(-0.102088475326202,-0.13602926811231,
0.227439542270961));
#18919=CARTESIAN_POINT('Ctrl Pts',(-0.169930093363525,0.00813139225995705,
0.219679566361962));
#18920=CARTESIAN_POINT('Ctrl Pts',(-0.0885810019960112,0.145257558931755,
0.211919590452965));
#18921=CARTESIAN_POINT('Ctrl Pts',(0.0705300022856002,0.154806449085219,
0.204159614543967));
#18922=CARTESIAN_POINT('Ctrl Pts',(0.167724284255384,0.0284781603319641,
0.196399638634969));
#18923=CARTESIAN_POINT('Ctrl Pts',(0.117670998255967,-0.122866343258294,
0.188639662725971));
#18924=CARTESIAN_POINT('Ctrl Pts',(-0.0356859920336591,-0.166337644224695,
0.180879686816973));
#18925=CARTESIAN_POINT('Ctrl Pts',(-0.157714277389017,-0.0637839670800676,
0.173119710907975));
#18926=CARTESIAN_POINT('Ctrl Pts',(-0.141283808251885,0.0947683240614489,
0.165359734998977));
#18927=CARTESIAN_POINT('Ctrl Pts',(-0.000819265566548849,0.17012162387625,
0.157599759089979));
#18928=CARTESIAN_POINT('Ctrl Pts',(0.140364559786514,0.0961244228297045,
0.149839783180981));
#18929=CARTESIAN_POINT('Ctrl Pts',(0.158321222407261,-0.0622614753404775,
0.142079807271983));
#18930=CARTESIAN_POINT('Ctrl Pts',(0.0372864568338413,-0.16598736897038,
0.134319831362986));
#18931=CARTESIAN_POINT('Ctrl Pts',(-0.116482378026109,-0.123991752606152,
0.126559855453987));
#18932=CARTESIAN_POINT('Ctrl Pts',(-0.167990437322196,0.0268572536432864,
0.11879987954499));
#18933=CARTESIAN_POINT('Ctrl Pts',(-0.0720183527756138,0.154128009733527,
0.111039903635992));
#18934=CARTESIAN_POINT('Ctrl Pts',(0.0871791483311938,0.146088660998552,
0.103279927726994));
#18935=CARTESIAN_POINT('Ctrl Pts',(0.169841505129784,0.00979680782987164,
0.0955199518179957));
#18936=CARTESIAN_POINT('Ctrl Pts',(0.103398469710631,-0.135095501656644,
0.0877599759089979));
#18937=CARTESIAN_POINT('Ctrl Pts',(-0.0538184879562023,-0.161386864625592,
0.08));
#18938=CARTESIAN_POINT('Ctrl Pts',(-0.163788539001263,-0.0459945892539838,
0.0722400240910021));
#18939=CARTESIAN_POINT('Ctrl Pts',(-0.129965899095288,0.10977507452059,
0.0644800481820042));
#18940=CARTESIAN_POINT('Ctrl Pts',(0.0179520450936897,0.169175430288133,
0.0567200722730062));
#18941=CARTESIAN_POINT('Ctrl Pts',(0.150115030399095,0.0800494771572726,
0.0489600963640084));
#18942=CARTESIAN_POINT('Ctrl Pts',(0.150480797316365,-0.0793413356316391,
0.0412001204550104));
#18943=CARTESIAN_POINT('Ctrl Pts',(0.0187574713458855,-0.169099111795828,
0.0334401445460125));
#18944=CARTESIAN_POINT('Ctrl Pts',(-0.129469733251211,-0.110362785133767,
0.0256801686370146));
#18945=CARTESIAN_POINT('Ctrl Pts',(-0.163964634349217,0.0451842589883535,
0.0179201927280167));
#18946=CARTESIAN_POINT('Ctrl Pts',(-0.0546483194245858,0.161212833824257,
0.0101602168190188));
#18947=CARTESIAN_POINT('Ctrl Pts',(0.10291452458962,0.135416470050577,0.00240024091002082));
#18948=CARTESIAN_POINT('Ctrl Pts',(0.147307246462226,0.0393999529324658,
-0.00277307636264439));
#18949=CARTESIAN_POINT('Ctrl Pts',(0.144813605913432,-0.00767158089707644,
-0.00535973499897704));
#18950=CARTESIAN_POINT('Ctrl Pts',(0.116913659442519,0.100696009035903,
0.256079204996931));
#18951=CARTESIAN_POINT('Ctrl Pts',(0.149644807637716,0.0626933279972582,
0.253492546360598));
#18952=CARTESIAN_POINT('Ctrl Pts',(0.174757532207842,-0.0470233419515556,
0.248319229087933));
#18953=CARTESIAN_POINT('Ctrl Pts',(0.0589061664806588,-0.171273640229548,
0.240559253178935));
#18954=CARTESIAN_POINT('Ctrl Pts',(-0.108623733429488,-0.144737267461644,
0.232799277269938));
#18955=CARTESIAN_POINT('Ctrl Pts',(-0.180808275411966,0.00865192846140473,
0.225039301360939));
#18956=CARTESIAN_POINT('Ctrl Pts',(-0.0942515706791253,0.154556313135293,
0.217279325451942));
#18957=CARTESIAN_POINT('Ctrl Pts',(0.0750450248431312,0.164716481511431,
0.209519349542944));
#18958=CARTESIAN_POINT('Ctrl Pts',(0.178461260043253,0.0303012077178856,
0.201759373633945));
#18959=CARTESIAN_POINT('Ctrl Pts',(0.125203781387627,-0.130731709675357,
0.193999397724948));
#18960=CARTESIAN_POINT('Ctrl Pts',(-0.0379704533096903,-0.17698585337688,
0.18623942181595));
#18961=CARTESIAN_POINT('Ctrl Pts',(-0.167810456277154,-0.0678671379413016,
0.178479445906952));
#18962=CARTESIAN_POINT('Ctrl Pts',(-0.150328180300649,0.100834978066992,
0.170719469997954));
#18963=CARTESIAN_POINT('Ctrl Pts',(-0.000871711368246156,0.181012066871201,
0.162959494088956));
#18964=CARTESIAN_POINT('Ctrl Pts',(0.149350085565286,0.102277888352765,
0.155199518179958));
#18965=CARTESIAN_POINT('Ctrl Pts',(0.168456255263351,-0.0662471829332422,
0.14743954227096));
#18966=CARTESIAN_POINT('Ctrl Pts',(0.0396733728729688,-0.17661315503135,
0.139679566361963));
#18967=CARTESIAN_POINT('Ctrl Pts',(-0.123939070884463,-0.131929162812062,
0.131919590452964));
#18968=CARTESIAN_POINT('Ctrl Pts',(-0.178744451066417,0.0285765376657333,
0.124159614543967));
#18969=CARTESIAN_POINT('Ctrl Pts',(-0.0766286530280003,0.163994611436961,
0.116399638634969));
#18970=CARTESIAN_POINT('Ctrl Pts',(0.0927599764682439,0.155440618724813,
0.108639662725971));
#18971=CARTESIAN_POINT('Ctrl Pts',(0.180714016146597,0.0104239566588842,
0.100879686816973));
#18972=CARTESIAN_POINT('Ctrl Pts',(0.11001758793024,-0.143743725357685,
0.093119710907975));
#18973=CARTESIAN_POINT('Ctrl Pts',(-0.0572637123892103,-0.171718146500831,
0.0853597349989769));
#18974=CARTESIAN_POINT('Ctrl Pts',(-0.174273565575645,-0.048938961879483,
0.0775997590899791));
#18975=CARTESIAN_POINT('Ctrl Pts',(-0.138285748054726,0.11680239511684,
0.0698397831809812));
#18976=CARTESIAN_POINT('Ctrl Pts',(0.0191012565771036,0.180005302104073,
0.0620798072719832));
#18977=CARTESIAN_POINT('Ctrl Pts',(0.159724738700703,0.0851738948996701,
0.0543198313629854));
#18978=CARTESIAN_POINT('Ctrl Pts',(0.160113920417758,-0.0844204212478698,
0.0465598554539874));
#18979=CARTESIAN_POINT('Ctrl Pts',(0.0199582426985643,-0.179924098035372,
0.0387998795449896));
#18980=CARTESIAN_POINT('Ctrl Pts',(-0.137757819841364,-0.117427728395404,
0.0310399036359917));
#18981=CARTESIAN_POINT('Ctrl Pts',(-0.174460933778308,0.0480767578110765,
0.0232799277269937));
#18982=CARTESIAN_POINT('Ctrl Pts',(-0.0581466660421577,0.171532975008042,
0.0155199518179959));
#18983=CARTESIAN_POINT('Ctrl Pts',(0.109502662757235,0.144085240745689,
0.00775997590899784));
#18984=CARTESIAN_POINT('Ctrl Pts',(0.156737212705124,0.0419221657566679,
0.00258665863633264));
#18985=CARTESIAN_POINT('Ctrl Pts',(0.15408394018464,-0.00816268198427004,
0.));
#18986=CARTESIAN_POINT('Ctrl Pts',(0.15408394018464,-0.00816268198427004,
0.));
#18987=CARTESIAN_POINT('Ctrl Pts',(0.153697863146473,0.00250812953454787,
1.45220469349306E-17));
#18988=CARTESIAN_POINT('Ctrl Pts',(0.152123106309386,0.0130673133993916,
-2.32988231788825E-17));
#18989=CARTESIAN_POINT('Ctrl Pts',(0.149466152202855,0.0233620190894148,
-6.07153216591882E-17));
#18990=CARTESIAN_POINT('Ctrl Pts',(0.14793019248835,0.0293132898222067,
-8.23454409684948E-17));
#18991=CARTESIAN_POINT('Ctrl Pts',(0.146031563681721,0.0351760135160456,
3.17823908273165E-17));
#18992=CARTESIAN_POINT('Ctrl Pts',(0.143784059453749,0.0409171473780902,
6.24500451351651E-17));
#18993=CARTESIAN_POINT('Ctrl Pts',(0.142595904075608,0.0439522291322952,
7.86626679846993E-17));
#18994=CARTESIAN_POINT('Ctrl Pts',(0.141309213132582,0.0469553015723855,
1.03399090950918E-16));
#18995=CARTESIAN_POINT('Ctrl Pts',(0.13992871365498,0.0499144025840292,
1.00613961606655E-16));
#18996=CARTESIAN_POINT('Ctrl Pts',(0.135493978469587,0.0594202586791481,
9.16669744478229E-17));
#18997=CARTESIAN_POINT('Ctrl Pts',(0.130119641392827,0.0684241765595774,
5.76730757846686E-17));
#18998=CARTESIAN_POINT('Ctrl Pts',(0.123887660540245,0.0767683201192124,
1.38777878078145E-16));
#18999=CARTESIAN_POINT('Ctrl Pts',(0.120656388342022,0.0810947453345699,
1.808305895663E-16));
#19000=CARTESIAN_POINT('Ctrl Pts',(0.117193874983239,0.0852432898306738,
1.062697842984E-16));
#19001=CARTESIAN_POINT('Ctrl Pts',(0.11350808038867,0.0891875047540603,
1.14491749414469E-16));
#19002=CARTESIAN_POINT('Ctrl Pts',(0.110158526423333,0.0927719043720516,
1.21963656801269E-16));
#19003=CARTESIAN_POINT('Ctrl Pts',(0.106618991420749,0.0961915975683434,
1.17223950247179E-16));
#19004=CARTESIAN_POINT('Ctrl Pts',(0.102922970874274,0.0994011657423757,
1.02348685082632E-16));
#19005=CARTESIAN_POINT('Ctrl Pts',(0.0973787571548163,0.104215676830788,
8.00350512245867E-17));
#19006=CARTESIAN_POINT('Ctrl Pts',(0.0914754811895955,0.108568278221023,
6.56075743842472E-17));
#19007=CARTESIAN_POINT('Ctrl Pts',(0.0852365492443714,0.11239450959967,
3.29597460435593E-17));
#19008=CARTESIAN_POINT('Ctrl Pts',(0.0787787796913796,0.116354950379705,
-7.26807264206779E-19));
#19009=CARTESIAN_POINT('Ctrl Pts',(0.0719608771003193,0.11975150351845,
7.81983513604452E-17));
#19010=CARTESIAN_POINT('Ctrl Pts',(0.0648645680501024,0.122569786811788,
1.05818132034585E-16));
#19011=CARTESIAN_POINT('Ctrl Pts',(0.0619760396963809,0.123716959397427,
1.17060669392563E-16));
#19012=CARTESIAN_POINT('Ctrl Pts',(0.0590419697559043,0.124767587801255,
-1.70921410850511E-17));
#19013=CARTESIAN_POINT('Ctrl Pts',(0.0560804949635964,0.12571697313192,
-8.67361737988404E-19));
#19014=CARTESIAN_POINT('Ctrl Pts',(0.0481895916857994,0.128246627558523,
4.23638569993146E-17));
#19015=CARTESIAN_POINT('Ctrl Pts',(0.040081547172159,0.13006877931966,2.48189907303608E-17));
#19016=CARTESIAN_POINT('Ctrl Pts',(0.0318655688619291,0.131172622122806,
0.));
#19017=CARTESIAN_POINT('Ctrl Pts',(0.0267717292715239,0.131856995664207,
-1.5387571972871E-17));
#19018=CARTESIAN_POINT('Ctrl Pts',(0.0216363184326117,0.132264755542675,
5.61228976213782E-17));
#19019=CARTESIAN_POINT('Ctrl Pts',(0.0164863123329273,0.132388468809724,
3.03576608295941E-17));
#19020=CARTESIAN_POINT('Ctrl Pts',(0.0120733572364389,0.13249447666326,
8.27985532573229E-18));
#19021=CARTESIAN_POINT('Ctrl Pts',(0.00764667637530932,0.132391154756805,
7.9933444120104E-17));
#19022=CARTESIAN_POINT('Ctrl Pts',(0.00324855819595315,0.132074892239241,
9.62771529167128E-17));
#19023=CARTESIAN_POINT('Ctrl Pts',(-0.00215998367955725,0.131685971569047,
1.16375665467493E-16));
#19024=CARTESIAN_POINT('Ctrl Pts',(-0.00753310453775717,0.130975837616781,
1.12286849362194E-16));
#19025=CARTESIAN_POINT('Ctrl Pts',(-0.0128378223015392,0.129936202211006,
1.27068494615301E-16));
#19026=CARTESIAN_POINT('Ctrl Pts',(-0.0180922709275414,0.128906418710228,
1.41710064449709E-16));
#19027=CARTESIAN_POINT('Ctrl Pts',(-0.023283936630727,0.12755123862641,
1.19281234835921E-16));
#19028=CARTESIAN_POINT('Ctrl Pts',(-0.028350637156304,0.125868914531291,
9.19403442267708E-17));
#19029=CARTESIAN_POINT('Ctrl Pts',(-0.0326437071621008,0.124443463179602,
6.87741127091605E-17));
#19030=CARTESIAN_POINT('Ctrl Pts',(-0.0368509055758185,0.122782751372096,
3.08039683582783E-17));
#19031=CARTESIAN_POINT('Ctrl Pts',(-0.0409513668396969,0.120880349084932,
-1.95156391047391E-18));
#19032=CARTESIAN_POINT('Ctrl Pts',(-0.0436523616789034,0.119627226953286,
-2.45035827619675E-17));
#19033=CARTESIAN_POINT('Ctrl Pts',(-0.0463070048384274,0.118269169850402,
-4.56986185075063E-18));
#19034=CARTESIAN_POINT('Ctrl Pts',(-0.0489111879062984,0.116810626195002,
-1.73472347597681E-18));
#19035=CARTESIAN_POINT('Ctrl Pts',(0.0958116152722397,0.0825211298936481,
0.24));
#19036=CARTESIAN_POINT('Ctrl Pts',(0.102494250906434,0.0762804363331629,
0.24));
#19037=CARTESIAN_POINT('Ctrl Pts',(0.108399952301676,0.0693089192431419,
0.24));
#19038=CARTESIAN_POINT('Ctrl Pts',(0.113520383394708,0.0617855200816623,
0.24));
#19039=CARTESIAN_POINT('Ctrl Pts',(0.11760088593285,0.0557900777417299,
0.24));
#19040=CARTESIAN_POINT('Ctrl Pts',(0.1211824537664,0.0494427873910869,0.24));
#19041=CARTESIAN_POINT('Ctrl Pts',(0.124247292533427,0.0428169095598754,
0.24));
#19042=CARTESIAN_POINT('Ctrl Pts',(0.125635784531567,0.0398151273949318,
0.24));
#19043=CARTESIAN_POINT('Ctrl Pts',(0.126914357096627,0.0367636074968772,
0.24));
#19044=CARTESIAN_POINT('Ctrl Pts',(0.128080244072735,0.0336751552254939,
0.24));
#19045=CARTESIAN_POINT('Ctrl Pts',(0.13155694143068,0.024465331227027,0.24));
#19046=CARTESIAN_POINT('Ctrl Pts',(0.134041462136676,0.0149150332268467,
0.24));
#19047=CARTESIAN_POINT('Ctrl Pts',(0.135496608205084,0.00520422800883078,
0.24));
#19048=CARTESIAN_POINT('Ctrl Pts',(0.136052940597398,0.00149158663520877,
0.24));
#19049=CARTESIAN_POINT('Ctrl Pts',(0.136458356591543,-0.00224482315054724,
0.24));
#19050=CARTESIAN_POINT('Ctrl Pts',(0.136708928272429,-0.00599574054845843,
0.24));
#19051=CARTESIAN_POINT('Ctrl Pts',(0.136894600108428,-0.00877514370161729,
0.24));
#19052=CARTESIAN_POINT('Ctrl Pts',(0.136994942037659,-0.0115613689854128,
0.24));
#19053=CARTESIAN_POINT('Ctrl Pts',(0.137008733057845,-0.0143405417274864,
0.24));
#19054=CARTESIAN_POINT('Ctrl Pts',(0.137045731231951,-0.0217964308202384,
0.24));
#19055=CARTESIAN_POINT('Ctrl Pts',(0.136462408227525,-0.0292204075226799,
0.24));
#19056=CARTESIAN_POINT('Ctrl Pts',(0.135240454646173,-0.0365388974416549,
0.24));
#19057=CARTESIAN_POINT('Ctrl Pts',(0.134058793448489,-0.0436160693529878,
0.24));
#19058=CARTESIAN_POINT('Ctrl Pts',(0.132280018312676,-0.050595007513092,
0.24));
#19059=CARTESIAN_POINT('Ctrl Pts',(0.129952822193542,-0.0574290655609092,
0.24));
#19060=CARTESIAN_POINT('Ctrl Pts',(0.128850070284018,-0.0606674134165377,
0.24));
#19061=CARTESIAN_POINT('Ctrl Pts',(0.127623182384127,-0.0638741644409745,
0.24));
#19062=CARTESIAN_POINT('Ctrl Pts',(0.126284110088584,-0.067028198101918,
0.24));
#19063=CARTESIAN_POINT('Ctrl Pts',(0.122654675969015,-0.0755769205431157,
0.24));
#19064=CARTESIAN_POINT('Ctrl Pts',(0.118195290975453,-0.0837663478860722,
0.24));
#19065=CARTESIAN_POINT('Ctrl Pts',(0.113014989178579,-0.0915013065162071,
0.24));
#19066=CARTESIAN_POINT('Ctrl Pts',(0.108985931714537,-0.0975172866704144,
0.24));
#19067=CARTESIAN_POINT('Ctrl Pts',(0.104519884911976,-0.103258562704539,
0.24));
#19068=CARTESIAN_POINT('Ctrl Pts',(0.0996546828651377,-0.108675969178894,
0.24));
#19069=CARTESIAN_POINT('Ctrl Pts',(0.0972822643803542,-0.11131765910988,
0.24));
#19070=CARTESIAN_POINT('Ctrl Pts',(0.09482095240722,-0.113875293456495,
0.24));
#19071=CARTESIAN_POINT('Ctrl Pts',(0.0922773332174137,-0.116342466058553,
0.24));
#19072=CARTESIAN_POINT('Ctrl Pts',(0.0868426048671788,-0.121613857680014,
0.24));
#19073=CARTESIAN_POINT('Ctrl Pts',(0.0810310485854155,-0.126474759557936,
0.24));
#19074=CARTESIAN_POINT('Ctrl Pts',(0.0748870600798396,-0.130870957562724,
0.24));
#19075=CARTESIAN_POINT('Ctrl Pts',(0.0715378781224404,-0.133267392228159,
0.24));
#19076=CARTESIAN_POINT('Ctrl Pts',(0.0680912231566627,-0.135524142754832,
0.24));
#19077=CARTESIAN_POINT('Ctrl Pts',(0.0645638484115253,-0.13762659390894,
0.24));
#19078=CARTESIAN_POINT('Ctrl Pts',(0.0598451535113139,-0.140439117742,0.24));
#19079=CARTESIAN_POINT('Ctrl Pts',(0.0549775790306604,-0.142978967531553,
0.24));
#19080=CARTESIAN_POINT('Ctrl Pts',(0.0499773507040556,-0.145225083935062,
0.24));
#19081=CARTESIAN_POINT('Ctrl Pts',(0.0466920976074369,-0.146700828718701,
0.24));
#19082=CARTESIAN_POINT('Ctrl Pts',(0.0433495270099635,-0.148049731670784,
0.24));
#19083=CARTESIAN_POINT('Ctrl Pts',(0.039956549802796,-0.149273502906639,
0.24));
#19084=CARTESIAN_POINT('Ctrl Pts',(-0.126296536029262,-6.10717992316628E-5,
0.159341967361942));
#19085=CARTESIAN_POINT('Ctrl Pts',(-0.12637083907321,-0.0163056929409037,
0.160361391877968));
#19086=CARTESIAN_POINT('Ctrl Pts',(-0.12344809088261,-0.0325245895549842,
0.161380816393994));
#19087=CARTESIAN_POINT('Ctrl Pts',(-0.117399968681154,-0.0474794518833934,
0.162400240910021));
#19088=CARTESIAN_POINT('Ctrl Pts',(-0.102053636235694,-0.0854254922118417,
0.164986899546353));
#19089=CARTESIAN_POINT('Ctrl Pts',(-0.0665853528586453,-0.115233359066084,
0.167573558182686));
#19090=CARTESIAN_POINT('Ctrl Pts',(-0.0265641275910804,-0.123819689910512,
0.170160216819019));
#19091=CARTESIAN_POINT('Ctrl Pts',(0.0134570976764845,-0.13240602075494,
0.172746875455351));
#19092=CARTESIAN_POINT('Ctrl Pts',(0.058031264834566,-0.119770815589554,
0.175333534091684));
#19093=CARTESIAN_POINT('Ctrl Pts',(0.0875924985281064,-0.0914586003428122,
0.177920192728017));
#19094=CARTESIAN_POINT('Ctrl Pts',(0.117153732221647,-0.0631463850960709,
0.180506851364349));
#19095=CARTESIAN_POINT('Ctrl Pts',(0.131702032450646,-0.0191571597679751,
0.183093510000682));
#19096=CARTESIAN_POINT('Ctrl Pts',(0.124851119980295,0.0211965060081854,
0.185680168637015));
#19097=CARTESIAN_POINT('Ctrl Pts',(0.118000207509943,0.0615501717843459,
0.188266827273347));
#19098=CARTESIAN_POINT('Ctrl Pts',(0.0897500823402403,0.0982682780085711,
0.19085348590968));
#19099=CARTESIAN_POINT('Ctrl Pts',(0.0525017161220023,0.115239608835997,
0.193440144546013));
#19100=CARTESIAN_POINT('Ctrl Pts',(0.0152533499037644,0.132210939663423,
0.196026803182345));
#19101=CARTESIAN_POINT('Ctrl Pts',(-0.030993257363009,0.129435495094051,
0.198613461818678));
#19102=CARTESIAN_POINT('Ctrl Pts',(-0.0659388717692058,0.108119484364762,
0.20120012045501));
#19103=CARTESIAN_POINT('Ctrl Pts',(-0.100884486175403,0.0868034736354726,
0.203786779091343));
#19104=CARTESIAN_POINT('Ctrl Pts',(-0.124529107721023,0.0469468967462671,
0.206373437727676));
#19105=CARTESIAN_POINT('Ctrl Pts',(-0.126492123469331,0.00606801008988057,
0.208960096364008));
#19106=CARTESIAN_POINT('Ctrl Pts',(-0.126588724127832,0.00405634646811867,
0.209087386696653));
#19107=CARTESIAN_POINT('Ctrl Pts',(-0.126632819376787,0.00204220716288977,
0.209214677029297));
#19108=CARTESIAN_POINT('Ctrl Pts',(-0.126625441102054,2.7778768752873E-5,
0.209341967361942));
#19109=CARTESIAN_POINT('Ctrl Pts',(-0.0398513841857245,-0.149064942821851,
0.24));
#19110=CARTESIAN_POINT('Ctrl Pts',(-0.0883048112969314,-0.136111285829332,
0.237413341363667));
#19111=CARTESIAN_POINT('Ctrl Pts',(-0.170871437255804,-0.0596187094618861,
0.232240024091002));
#19112=CARTESIAN_POINT('Ctrl Pts',(-0.145169204726118,0.108307533342445,
0.224480048182004));
#19113=CARTESIAN_POINT('Ctrl Pts',(0.00818767200092134,0.180778621679153,
0.216720072273006));
#19114=CARTESIAN_POINT('Ctrl Pts',(0.154249898498561,0.0947283641859207,
0.208960096364008));
#19115=CARTESIAN_POINT('Ctrl Pts',(0.164950538597243,-0.0745810526211722,
0.201200120455011));
#19116=CARTESIAN_POINT('Ctrl Pts',(0.0308106631569891,-0.178364693496558,
0.193440144546012));
#19117=CARTESIAN_POINT('Ctrl Pts',(-0.13036283225522,-0.125587074703769,
0.185680168637015));
#19118=CARTESIAN_POINT('Ctrl Pts',(-0.17709781441264,0.03745832727601,0.177920192728017));
#19119=CARTESIAN_POINT('Ctrl Pts',(-0.0683530255288039,0.167611467503216,
0.170160216819019));
#19120=CARTESIAN_POINT('Ctrl Pts',(0.100397202365132,0.150621028353064,
0.162400240910021));
#19121=CARTESIAN_POINT('Ctrl Pts',(0.18100910679194,0.00139719974911195,
0.154640265001023));
#19122=CARTESIAN_POINT('Ctrl Pts',(0.102711092909207,-0.149052183789333,
0.146880289092025));
#19123=CARTESIAN_POINT('Ctrl Pts',(-0.0657574679958034,-0.168648048308422,
0.139120313183027));
#19124=CARTESIAN_POINT('Ctrl Pts',(-0.176497206835689,-0.0401861834345609,
0.131360337274029));
#19125=CARTESIAN_POINT('Ctrl Pts',(-0.132288575936487,0.123555290563421,
0.123600361365031));
#19126=CARTESIAN_POINT('Ctrl Pts',(0.0280571680938306,0.178826694862324,
0.115840385456033));
#19127=CARTESIAN_POINT('Ctrl Pts',(0.163771354656592,0.0771047007047774,
0.108080409547035));
#19128=CARTESIAN_POINT('Ctrl Pts',(0.155709331479018,-0.0923080778690166,
0.100320433638038));
#19129=CARTESIAN_POINT('Ctrl Pts',(0.0109489686262093,-0.180682908560435,
0.0925604577290397));
#19130=CARTESIAN_POINT('Ctrl Pts',(-0.143423754439364,-0.110434756566834,
0.0848004818200417));
#19131=CARTESIAN_POINT('Ctrl Pts',(-0.17188331593326,0.0567648465404429,
0.0770405059110439));
#19132=CARTESIAN_POINT('Ctrl Pts',(-0.0494457976037486,0.174130301808973,
0.0692805300020459));
#19133=CARTESIAN_POINT('Ctrl Pts',(0.11640175885633,0.13862511662766,0.061520554093048));
#19134=CARTESIAN_POINT('Ctrl Pts',(0.18005704388064,-0.0185795878987759,
0.0537605781840501));
#19135=CARTESIAN_POINT('Ctrl Pts',(0.0856431484406112,-0.159474177462153,
0.0460006022750521));
#19136=CARTESIAN_POINT('Ctrl Pts',(-0.0839657292871194,-0.160363143120653,
0.0382406263660544));
#19137=CARTESIAN_POINT('Ctrl Pts',(-0.179844832231877,-0.0204718628801216,
0.0304806504570563));
#19138=CARTESIAN_POINT('Ctrl Pts',(-0.117866479118068,0.137399078213474,
0.0227206745480585));
#19139=CARTESIAN_POINT('Ctrl Pts',(0.0476444145610997,0.174632482457551,
0.0149606986390605));
#19140=CARTESIAN_POINT('Ctrl Pts',(0.171219786572432,0.0585809927800803,
0.00720072273006264));
#19141=CARTESIAN_POINT('Ctrl Pts',(0.144688050375066,-0.108949473877577,
-0.000559253178935319));
#19142=CARTESIAN_POINT('Ctrl Pts',(-0.0092814439579932,-0.180735423716049,
-0.00831922908793317));
#19143=CARTESIAN_POINT('Ctrl Pts',(-0.105867686800049,-0.122947365648507,
-0.0134925463605985));
#19144=CARTESIAN_POINT('Ctrl Pts',(-0.131895903200816,-0.0800747195988904,
-0.0160792049969312));
#19145=CARTESIAN_POINT('Ctrl Pts',(-0.0374537582415196,-0.140096572423086,
0.245359734998977));
#19146=CARTESIAN_POINT('Ctrl Pts',(-0.0829920245295529,-0.127922261611689,
0.242773076362644));
#19147=CARTESIAN_POINT('Ctrl Pts',(-0.160591096949962,-0.0560317985556137,
0.237599759089979));
#19148=CARTESIAN_POINT('Ctrl Pts',(-0.13643521822445,0.101791299158848,
0.229839783180981));
#19149=CARTESIAN_POINT('Ctrl Pts',(0.00769506740980954,0.1699022237233,
0.222079807271983));
#19150=CARTESIAN_POINT('Ctrl Pts',(0.144969579481095,0.0890291096113304,
0.214319831362985));
#19151=CARTESIAN_POINT('Ctrl Pts',(0.155026424317845,-0.0700939445729984,
0.206559855453987));
#19152=CARTESIAN_POINT('Ctrl Pts',(0.0289569648011409,-0.167633527556011,
0.19879987954499));
#19153=CARTESIAN_POINT('Ctrl Pts',(-0.122519659046519,-0.118031231043151,
0.191039903635991));
#19154=CARTESIAN_POINT('Ctrl Pts',(-0.166442869216287,0.0352046776440443,
0.183279927726994));
#19155=CARTESIAN_POINT('Ctrl Pts',(-0.064240621638164,0.157527260611955,
0.175519951817996));
#19156=CARTESIAN_POINT('Ctrl Pts',(0.0943568867767351,0.141559037340679,
0.167759975908998));
#19157=CARTESIAN_POINT('Ctrl Pts',(0.170118841887737,0.00131313836865665,
0.16));
#19158=CARTESIAN_POINT('Ctrl Pts',(0.0965315639882279,-0.140084581027326,
0.152240024091002));
#19159=CARTESIAN_POINT('Ctrl Pts',(-0.0618012237018238,-0.158501476380598,
0.144480048182004));
#19160=CARTESIAN_POINT('Ctrl Pts',(-0.165878396703103,-0.0377684145673052,
0.136720072273006));
#19161=CARTESIAN_POINT('Ctrl Pts',(-0.124329541933827,0.116121687534276,
0.128960096364008));
#19162=CARTESIAN_POINT('Ctrl Pts',(0.0263691315170036,0.168067732987372,
0.12120012045501));
#19163=CARTESIAN_POINT('Ctrl Pts',(0.153918185014798,0.0724657594331675,
0.113440144546012));
#19164=CARTESIAN_POINT('Ctrl Pts',(0.146341206869619,-0.0867544378416841,
0.105680168637015));
#19165=CARTESIAN_POINT('Ctrl Pts',(0.0102902328814698,-0.169812269106107,
0.0979201927280167));
#19166=CARTESIAN_POINT('Ctrl Pts',(-0.134794781526993,-0.103790539737311,
0.0901602168190187));
#19167=CARTESIAN_POINT('Ctrl Pts',(-0.161542096774173,0.0533496359633175,
0.0824002409100209));
#19168=CARTESIAN_POINT('Ctrl Pts',(-0.0464709316213242,0.163653894581969,
0.074640265001023));
#19169=CARTESIAN_POINT('Ctrl Pts',(0.109398542213106,0.130284849835523,
0.066880289092025));
#19170=CARTESIAN_POINT('Ctrl Pts',(0.16922405906302,-0.0174617621848401,
0.0591203131830272));
#19171=CARTESIAN_POINT('Ctrl Pts',(0.0804904984426183,-0.149879543972585,
0.0513603372740291));
#19172=CARTESIAN_POINT('Ctrl Pts',(-0.0789139998409189,-0.150715025739123,
0.0436003613650314));
#19173=CARTESIAN_POINT('Ctrl Pts',(-0.169024614954586,-0.0192401899891918,
0.0358403854560333));
#19174=CARTESIAN_POINT('Ctrl Pts',(-0.110775138777956,0.12913257502003,
0.0280804095470356));
#19175=CARTESIAN_POINT('Ctrl Pts',(0.0447779273164969,0.164125861942445,
0.0203204336380375));
#19176=CARTESIAN_POINT('Ctrl Pts',(0.16091848811479,0.0550565152494576,
0.0125604577290397));
#19177=CARTESIAN_POINT('Ctrl Pts',(0.135983012131502,-0.10239461786658,
0.00480048182004171));
#19178=CARTESIAN_POINT('Ctrl Pts',(-0.00872303347143,-0.169861624730324,
-0.00295949408895612));
#19179=CARTESIAN_POINT('Ctrl Pts',(-0.0994982439886826,-0.115550337924785,
-0.00813281136162148));
#19180=CARTESIAN_POINT('Ctrl Pts',(-0.123960494032221,-0.0752570895690155,
-0.0107194699979541));
#19181=CARTESIAN_POINT('Ctrl Pts',(-0.0350561322973148,-0.13112820202432,
0.250719469997954));
#19182=CARTESIAN_POINT('Ctrl Pts',(-0.0776792377621743,-0.119733237394047,
0.248132811361621));
#19183=CARTESIAN_POINT('Ctrl Pts',(-0.150310756644121,-0.0524448876493412,
0.242959494088956));
#19184=CARTESIAN_POINT('Ctrl Pts',(-0.127701231722781,0.0952750649752511,
0.235199518179958));
#19185=CARTESIAN_POINT('Ctrl Pts',(0.00720246281869772,0.159025825767447,
0.22743954227096));
#19186=CARTESIAN_POINT('Ctrl Pts',(0.135689260463629,0.08332985503674,0.219679566361962));
#19187=CARTESIAN_POINT('Ctrl Pts',(0.145102310038447,-0.0656068365248246,
0.211919590452964));
#19188=CARTESIAN_POINT('Ctrl Pts',(0.0271032664452926,-0.156902361615465,
0.204159614543967));
#19189=CARTESIAN_POINT('Ctrl Pts',(-0.114676485837817,-0.110475387382534,
0.196399638634969));
#19190=CARTESIAN_POINT('Ctrl Pts',(-0.155787924019933,0.0329510280120788,
0.188639662725971));
#19191=CARTESIAN_POINT('Ctrl Pts',(-0.0601282177475243,0.147443053720694,
0.180879686816973));
#19192=CARTESIAN_POINT('Ctrl Pts',(0.0883165711883383,0.132497046328295,
0.173119710907975));
#19193=CARTESIAN_POINT('Ctrl Pts',(0.159228576983534,0.00122907698820117,
0.165359734998977));
#19194=CARTESIAN_POINT('Ctrl Pts',(0.0903520350672485,-0.131116978265319,
0.157599759089979));
#19195=CARTESIAN_POINT('Ctrl Pts',(-0.0578449794078444,-0.148354904452775,
0.149839783180981));
#19196=CARTESIAN_POINT('Ctrl Pts',(-0.155259586570517,-0.0353506457000499,
0.142079807271983));
#19197=CARTESIAN_POINT('Ctrl Pts',(-0.116370507931168,0.108688084505131,
0.134319831362985));
#19198=CARTESIAN_POINT('Ctrl Pts',(0.0246810949401768,0.157308771112418,
0.126559855453988));
#19199=CARTESIAN_POINT('Ctrl Pts',(0.144065015373005,0.0678268181615582,
0.118799879544989));
#19200=CARTESIAN_POINT('Ctrl Pts',(0.13697308226022,-0.0812007978143519,
0.111039903635992));
#19201=CARTESIAN_POINT('Ctrl Pts',(0.00963149713673027,-0.15894162965178,
0.103279927726994));
#19202=CARTESIAN_POINT('Ctrl Pts',(-0.126165808614623,-0.0971463229077874,
0.0955199518179957));
#19203=CARTESIAN_POINT('Ctrl Pts',(-0.151200877615086,0.0499344253861922,
0.087759975908998));
#19204=CARTESIAN_POINT('Ctrl Pts',(-0.0434960656388994,0.153177487354966,
0.08));
#19205=CARTESIAN_POINT('Ctrl Pts',(0.102395325569881,0.121944583043386,
0.072240024091002));
#19206=CARTESIAN_POINT('Ctrl Pts',(0.158391074245402,-0.0163439364709043,
0.0644800481820042));
#19207=CARTESIAN_POINT('Ctrl Pts',(0.0753378484446251,-0.140284910483017,
0.0567200722730062));
#19208=CARTESIAN_POINT('Ctrl Pts',(-0.0738622703947183,-0.141066908357593,
0.0489600963640083));
#19209=CARTESIAN_POINT('Ctrl Pts',(-0.158204397677296,-0.018008517098262,
0.0412001204550104));
#19210=CARTESIAN_POINT('Ctrl Pts',(-0.103683798437843,0.120866071826586,
0.0334401445460125));
#19211=CARTESIAN_POINT('Ctrl Pts',(0.0419114400718942,0.153619241427338,
0.0256801686370146));
#19212=CARTESIAN_POINT('Ctrl Pts',(0.150617189657149,0.051532037718835,
0.0179201927280167));
#19213=CARTESIAN_POINT('Ctrl Pts',(0.127277973887939,-0.0958397618555833,
0.0101602168190187));
#19214=CARTESIAN_POINT('Ctrl Pts',(-0.00816462298486686,-0.1589878257446,
0.00240024091002091));
#19215=CARTESIAN_POINT('Ctrl Pts',(-0.0931288011773165,-0.108153310201063,
-0.00277307636264444));
#19216=CARTESIAN_POINT('Ctrl Pts',(-0.116025084863626,-0.0704394595391406,
-0.00535973499897709));
#19217=CARTESIAN_POINT('Ctrl Pts',(-0.0326585063531099,-0.122159831625555,
0.256079204996931));
#19218=CARTESIAN_POINT('Ctrl Pts',(-0.0723664509947957,-0.111544213176404,
0.253492546360598));
#19219=CARTESIAN_POINT('Ctrl Pts',(-0.140030416338279,-0.0488579767430688,
0.248319229087933));
#19220=CARTESIAN_POINT('Ctrl Pts',(-0.118967245221113,0.0887588307916541,
0.240559253178936));
#19221=CARTESIAN_POINT('Ctrl Pts',(0.00670985822758596,0.148149427811594,
0.232799277269937));
#19222=CARTESIAN_POINT('Ctrl Pts',(0.126408941446163,0.0776306004621497,
0.225039301360939));
#19223=CARTESIAN_POINT('Ctrl Pts',(0.13517819575905,-0.0611197284766509,
0.217279325451942));
#19224=CARTESIAN_POINT('Ctrl Pts',(0.0252495680894444,-0.146171195674918,
0.209519349542944));
#19225=CARTESIAN_POINT('Ctrl Pts',(-0.106833312629116,-0.102919543721916,
0.201759373633946));
#19226=CARTESIAN_POINT('Ctrl Pts',(-0.14513297882358,0.0306973783801131,
0.193999397724948));
#19227=CARTESIAN_POINT('Ctrl Pts',(-0.0560158138568844,0.137358846829434,
0.18623942181595));
#19228=CARTESIAN_POINT('Ctrl Pts',(0.0822762555999414,0.12343505531591,
0.178479445906952));
#19229=CARTESIAN_POINT('Ctrl Pts',(0.148338312079331,0.00114501560774606,
0.170719469997954));
#19230=CARTESIAN_POINT('Ctrl Pts',(0.0841725061462688,-0.122149375503312,
0.162959494088956));
#19231=CARTESIAN_POINT('Ctrl Pts',(-0.0538887351138648,-0.138208332524951,
0.155199518179959));
#19232=CARTESIAN_POINT('Ctrl Pts',(-0.144640776437932,-0.0329328768327946,
0.14743954227096));
#19233=CARTESIAN_POINT('Ctrl Pts',(-0.108411473928508,0.101254481475986,
0.139679566361963));
#19234=CARTESIAN_POINT('Ctrl Pts',(0.0229930583633497,0.146549809237466,
0.131919590452964));
#19235=CARTESIAN_POINT('Ctrl Pts',(0.134211845731212,0.0631878768899486,
0.124159614543967));
#19236=CARTESIAN_POINT('Ctrl Pts',(0.127604957650822,-0.0756471577870196,
0.116399638634969));
#19237=CARTESIAN_POINT('Ctrl Pts',(0.00897276139199077,-0.148070990197453,
0.108639662725971));
#19238=CARTESIAN_POINT('Ctrl Pts',(-0.117536835702253,-0.0905021060782641,
0.100879686816973));
#19239=CARTESIAN_POINT('Ctrl Pts',(-0.140859658455999,0.0465192148090667,
0.0931197109079749));
#19240=CARTESIAN_POINT('Ctrl Pts',(-0.0405211996564747,0.142701080127962,
0.0853597349989771));
#19241=CARTESIAN_POINT('Ctrl Pts',(0.0953921089266558,0.113604316251249,
0.077599759089979));
#19242=CARTESIAN_POINT('Ctrl Pts',(0.147558089427783,-0.0152261107569683,
0.0698397831809813));
#19243=CARTESIAN_POINT('Ctrl Pts',(0.070185198446632,-0.130690276993449,
0.0620798072719832));
#19244=CARTESIAN_POINT('Ctrl Pts',(-0.0688105409485176,-0.131418790976063,
0.0543198313629854));
#19245=CARTESIAN_POINT('Ctrl Pts',(-0.147384180400005,-0.0167768442073323,
0.0465598554539874));
#19246=CARTESIAN_POINT('Ctrl Pts',(-0.0965924580977301,0.112599568633142,
0.0387998795449896));
#19247=CARTESIAN_POINT('Ctrl Pts',(0.0390449528272914,0.143112620912232,
0.0310399036359916));
#19248=CARTESIAN_POINT('Ctrl Pts',(0.140315891199508,0.0480075601882123,
0.0232799277269937));
#19249=CARTESIAN_POINT('Ctrl Pts',(0.118572935644375,-0.0892849058445864,
0.0155199518179958));
#19250=CARTESIAN_POINT('Ctrl Pts',(-0.00760621249830358,-0.148114026758875,
0.00775997590899793));
#19251=CARTESIAN_POINT('Ctrl Pts',(-0.0867593583659504,-0.100756282477341,
0.00258665863633259));
#19252=CARTESIAN_POINT('Ctrl Pts',(-0.108089675695031,-0.0656218295092657,
-5.55111512312578E-17));
#19253=CARTESIAN_POINT('Ctrl Pts',(-0.108089675695031,-0.0656218295092657,
-5.55111512312578E-17));
#19254=CARTESIAN_POINT('Ctrl Pts',(-0.104219465379748,-0.0739058869203245,
-4.02841154597017E-17));
#19255=CARTESIAN_POINT('Ctrl Pts',(-0.0994141168358061,-0.0816768736924768,
-5.16144647363644E-17));
#19256=CARTESIAN_POINT('Ctrl Pts',(-0.0938412360364922,-0.088871564406415,
-3.81639164714898E-17));
#19257=CARTESIAN_POINT('Ctrl Pts',(-0.0894001862863345,-0.094605040600905,
-2.74451237748006E-17));
#19258=CARTESIAN_POINT('Ctrl Pts',(-0.0844703330957707,-0.0999727304469881,
3.12377098840079E-17));
#19259=CARTESIAN_POINT('Ctrl Pts',(-0.0791158513129458,-0.104935071387697,
-1.21430643318376E-17));
#19260=CARTESIAN_POINT('Ctrl Pts',(-0.0766900604813501,-0.107183206995485,
-3.17962611543325E-17));
#19261=CARTESIAN_POINT('Ctrl Pts',(-0.0741829996358932,-0.109342173006691,
4.83248416902999E-17));
#19262=CARTESIAN_POINT('Ctrl Pts',(-0.0716059924168524,-0.111405381598006,
5.3776427755281E-17));
#19263=CARTESIAN_POINT('Ctrl Pts',(-0.0639212992135713,-0.117557915794061,
7.00331794132204E-17));
#19264=CARTESIAN_POINT('Ctrl Pts',(-0.0556061968393146,-0.12287204611112,
-5.69073736333764E-18));
#19265=CARTESIAN_POINT('Ctrl Pts',(-0.0468203466856493,-0.127256781127915,
5.55111512312578E-17));
#19266=CARTESIAN_POINT('Ctrl Pts',(-0.0434613267337519,-0.12893315986732,
7.89099528597243E-17));
#19267=CARTESIAN_POINT('Ctrl Pts',(-0.0400330653128497,-0.130473352587733,
3.97002991909352E-17));
#19268=CARTESIAN_POINT('Ctrl Pts',(-0.0365431560942257,-0.131870761756357,
6.59194920871187E-17));
#19269=CARTESIAN_POINT('Ctrl Pts',(-0.0339571636773035,-0.13290622981212,
8.5347686277821E-17));
#19270=CARTESIAN_POINT('Ctrl Pts',(-0.0313383144727484,-0.133862652235137,
-2.74403076010104E-17));
#19271=CARTESIAN_POINT('Ctrl Pts',(-0.0286994266230122,-0.134734580282325,
-2.42861286636753E-17));
#19272=CARTESIAN_POINT('Ctrl Pts',(-0.0216199050576346,-0.137073760181214,
-1.58242011095522E-17));
#19273=CARTESIAN_POINT('Ctrl Pts',(-0.0143790427459088,-0.138813119073991,
5.80198461902811E-17));
#19274=CARTESIAN_POINT('Ctrl Pts',(-0.0070411538297537,-0.139912507657099,
6.93889390390723E-17));
#19275=CARTESIAN_POINT('Ctrl Pts',(5.47883476400097E-5,-0.140975646920361,
8.02325614020808E-17));
#19276=CARTESIAN_POINT('Ctrl Pts',(0.00724182591717642,-0.141440539972256,
1.32011341321413E-16));
#19277=CARTESIAN_POINT('Ctrl Pts',(0.0144605478337719,-0.141339082434075,
1.61329283265843E-16));
#19278=CARTESIAN_POINT('Ctrl Pts',(0.0178811722145177,-0.141291006315792,
1.75221724083914E-16));
#19279=CARTESIAN_POINT('Ctrl Pts',(0.021310106848269,-0.141115105569205,
1.85534911235541E-16));
#19280=CARTESIAN_POINT('Ctrl Pts',(0.0247235715439624,-0.140816220288761,
1.71737624121704E-16));
#19281=CARTESIAN_POINT('Ctrl Pts',(0.0339754553361668,-0.140006119078294,
1.34341339582434E-16));
#19282=CARTESIAN_POINT('Ctrl Pts',(0.0431421008898472,-0.138295657968001,
8.04496487960062E-17));
#19283=CARTESIAN_POINT('Ctrl Pts',(0.0520992976556894,-0.135759125106636,
3.20923843055709E-17));
#19284=CARTESIAN_POINT('Ctrl Pts',(0.0590658916121619,-0.13378629867842,
-5.518202506064E-18));
#19285=CARTESIAN_POINT('Ctrl Pts',(0.0659062642374416,-0.131312982137409,
7.87850579480063E-17));
#19286=CARTESIAN_POINT('Ctrl Pts',(0.0725619642951071,-0.128359965266718,
7.63278329429795E-17));
#19287=CARTESIAN_POINT('Ctrl Pts',(0.0758074813473741,-0.126919986522721,
7.51296170399226E-17));
#19288=CARTESIAN_POINT('Ctrl Pts',(0.0790005264283722,-0.125369490597537,
8.38688896655138E-17));
#19289=CARTESIAN_POINT('Ctrl Pts',(0.0821329715644795,-0.123712761836801,
7.24247051220317E-17));
#19290=CARTESIAN_POINT('Ctrl Pts',(0.0888257654942848,-0.120172989003949,
4.79730178566093E-17));
#19291=CARTESIAN_POINT('Ctrl Pts',(0.0952446087626691,-0.116147988031934,
8.96774285244103E-17));
#19292=CARTESIAN_POINT('Ctrl Pts',(0.101324221742587,-0.111663228753314,
8.28330459778925E-17));
#19293=CARTESIAN_POINT('Ctrl Pts',(0.104638321741973,-0.109218510516871,
7.91020571356516E-17));
#19294=CARTESIAN_POINT('Ctrl Pts',(0.107849695272814,-0.106637925639498,
3.17151869302413E-17));
#19295=CARTESIAN_POINT('Ctrl Pts',(0.110939265073957,-0.10393289123317,
1.53956708492942E-17));
#19296=CARTESIAN_POINT('Ctrl Pts',(0.115072333360666,-0.100314234708527,
-6.43574216607592E-18));
#19297=CARTESIAN_POINT('Ctrl Pts',(0.118992075260627,-0.0964697210975667,
5.54296751400654E-17));
#19298=CARTESIAN_POINT('Ctrl Pts',(0.122673447199167,-0.0924082746861152,
3.52365706057789E-17));
#19299=CARTESIAN_POINT('Ctrl Pts',(0.125092164655522,-0.0897398425098966,
2.31620156359627E-17));
#19300=CARTESIAN_POINT('Ctrl Pts',(0.127407959881093,-0.0869777021544565,
-4.01489640485901E-17));
#19301=CARTESIAN_POINT('Ctrl Pts',(0.129620323775263,-0.0841289546921697,
-3.98986399474666E-17));
#19302=CARTESIAN_POINT('Ctrl Pts',(-0.126471935391749,0.000101176582396995,
0.195658032638058));
#19303=CARTESIAN_POINT('Ctrl Pts',(-0.126547267107008,0.00888033934128026,
0.195105154333688));
#19304=CARTESIAN_POINT('Ctrl Pts',(-0.125707148272093,0.0176451944231377,
0.194552276029318));
#19305=CARTESIAN_POINT('Ctrl Pts',(-0.12389684029672,0.0262048027713284,
0.193999397724948));
#19306=CARTESIAN_POINT('Ctrl Pts',(-0.115427257168015,0.0662512011965534,
0.191412739088615));
#19307=CARTESIAN_POINT('Ctrl Pts',(-0.0857215355124495,0.101805024012994,
0.188826080452282));
#19308=CARTESIAN_POINT('Ctrl Pts',(-0.0478199964418627,0.117261303502293,
0.18623942181595));
#19309=CARTESIAN_POINT('Ctrl Pts',(-0.0099184573712758,0.132717582991593,
0.183652763179617));
#19310=CARTESIAN_POINT('Ctrl Pts',(0.0361788991143328,0.128076319153751,
0.181066104543285));
#19311=CARTESIAN_POINT('Ctrl Pts',(0.070237920103702,0.105374013950137,
0.178479445906952));
#19312=CARTESIAN_POINT('Ctrl Pts',(0.104296941093071,0.0826717087465222,
0.175892787270619));
#19313=CARTESIAN_POINT('Ctrl Pts',(0.126317626586201,0.0419083621771342,
0.173306128634287));
#19314=CARTESIAN_POINT('Ctrl Pts',(0.126633668343922,0.000977623707263797,
0.170719469997954));
#19315=CARTESIAN_POINT('Ctrl Pts',(0.126949710101644,-0.0399531147626067,
0.168132811361621));
#19316=CARTESIAN_POINT('Ctrl Pts',(0.105561108123956,-0.08105124513296,
0.165546152725289));
#19317=CARTESIAN_POINT('Ctrl Pts',(0.0718566002584231,-0.104276803155076,
0.162959494088956));
#19318=CARTESIAN_POINT('Ctrl Pts',(0.0381520923928904,-0.127502361177192,
0.160372835452623));
#19319=CARTESIAN_POINT('Ctrl Pts',(-0.00786832136048696,-0.132855346851071,
0.157786176816291));
#19320=CARTESIAN_POINT('Ctrl Pts',(-0.0460038684578537,-0.117985930405985,
0.155199518179958));
#19321=CARTESIAN_POINT('Ctrl Pts',(-0.0841394155552204,-0.103116513960899,
0.152612859543626));
#19322=CARTESIAN_POINT('Ctrl Pts',(-0.114390095996576,-0.0680246953968468,
0.150026200907293));
#19323=CARTESIAN_POINT('Ctrl Pts',(-0.12347721913235,-0.0281142263966907,
0.14743954227096));
#19324=CARTESIAN_POINT('Ctrl Pts',(-0.125563410841138,-0.018951712774069,
0.14684570572666));
#19325=CARTESIAN_POINT('Ctrl Pts',(-0.126534167537385,-0.00953522996602069,
0.146251869182359));
#19326=CARTESIAN_POINT('Ctrl Pts',(-0.126453631260982,-0.000102348163238207,
0.145658032638058));
#19327=CARTESIAN_POINT('Ctrl Pts',(-0.0398513841857245,-0.149064942821851,
0.24));
#19328=CARTESIAN_POINT('Ctrl Pts',(-0.0498806325786677,-0.145400296738327,
0.24));
#19329=CARTESIAN_POINT('Ctrl Pts',(-0.0594363948008725,-0.140639648297949,
0.24));
#19330=CARTESIAN_POINT('Ctrl Pts',(-0.0684062055177017,-0.134931499399492,
0.24));
#19331=CARTESIAN_POINT('Ctrl Pts',(-0.0735915624001909,-0.131631676235849,
0.24));
#19332=CARTESIAN_POINT('Ctrl Pts',(-0.0785806353345173,-0.128014298080738,
0.24));
#19333=CARTESIAN_POINT('Ctrl Pts',(-0.0833462611484583,-0.124102693747304,
0.24));
#19334=CARTESIAN_POINT('Ctrl Pts',(-0.0858656342542594,-0.122034803580736,
0.24));
#19335=CARTESIAN_POINT('Ctrl Pts',(-0.0883241156266364,-0.11988309220465,
0.24));
#19336=CARTESIAN_POINT('Ctrl Pts',(-0.0907117892851122,-0.117655751751618,
0.24));
#19337=CARTESIAN_POINT('Ctrl Pts',(-0.0983819858496404,-0.110500611839494,
0.24));
#19338=CARTESIAN_POINT('Ctrl Pts',(-0.105284458416918,-0.102606966330569,
0.24));
#19339=CARTESIAN_POINT('Ctrl Pts',(-0.111294422020379,-0.0941015332659665,
0.24));
#19340=CARTESIAN_POINT('Ctrl Pts',(-0.114410577497229,-0.0896914812962706,
0.24));
#19341=CARTESIAN_POINT('Ctrl Pts',(-0.117286101138547,-0.0851164738413172,
0.24));
#19342=CARTESIAN_POINT('Ctrl Pts',(-0.119898298320422,-0.0803922539627851,
0.24));
#19343=CARTESIAN_POINT('Ctrl Pts',(-0.1222721977331,-0.0760990011896685,
0.24));
#19344=CARTESIAN_POINT('Ctrl Pts',(-0.124430744329062,-0.0716759619599862,
0.24));
#19345=CARTESIAN_POINT('Ctrl Pts',(-0.126341093034125,-0.0671690272221462,
0.24));
#19346=CARTESIAN_POINT('Ctrl Pts',(-0.129206708925078,-0.060408406100978,
0.24));
#19347=CARTESIAN_POINT('Ctrl Pts',(-0.131522065955468,-0.0534490321795157,
0.24));
#19348=CARTESIAN_POINT('Ctrl Pts',(-0.133233091500091,-0.0463330844490581,
0.24));
#19349=CARTESIAN_POINT('Ctrl Pts',(-0.135004134506116,-0.0389675313754268,
0.24));
#19350=CARTESIAN_POINT('Ctrl Pts',(-0.136127599829873,-0.0314337185245799,
0.24));
#19351=CARTESIAN_POINT('Ctrl Pts',(-0.136615064298196,-0.0238138180582873,
0.24));
#19352=CARTESIAN_POINT('Ctrl Pts',(-0.136813484749433,-0.0207121682209076,
0.24));
#19353=CARTESIAN_POINT('Ctrl Pts',(-0.136906013213758,-0.0175970392000076,
0.24));
#19354=CARTESIAN_POINT('Ctrl Pts',(-0.136893785357156,-0.0144871321155608,
0.24));
#19355=CARTESIAN_POINT('Ctrl Pts',(-0.136861203984761,-0.00620072149302863,
0.24));
#19356=CARTESIAN_POINT('Ctrl Pts',(-0.136088646936857,0.00207357465703332,
0.24));
#19357=CARTESIAN_POINT('Ctrl Pts',(-0.134599584032292,0.0102285531249486,
0.24));
#19358=CARTESIAN_POINT('Ctrl Pts',(-0.133676409755049,0.0152843948425598,
0.24));
#19359=CARTESIAN_POINT('Ctrl Pts',(-0.132477333465274,0.0202942984003417,
0.24));
#19360=CARTESIAN_POINT('Ctrl Pts',(-0.131003622030167,0.0252303138624672,
0.24));
#19361=CARTESIAN_POINT('Ctrl Pts',(-0.129740734874544,0.029460199292259,
0.24));
#19362=CARTESIAN_POINT('Ctrl Pts',(-0.128274507607502,0.0336384499732856,
0.24));
#19363=CARTESIAN_POINT('Ctrl Pts',(-0.126614574688298,0.0377237273426867,
0.24));
#19364=CARTESIAN_POINT('Ctrl Pts',(-0.124573382985647,0.042747324485064,
0.24));
#19365=CARTESIAN_POINT('Ctrl Pts',(-0.122237651925267,0.0476379767326878,
0.24));
#19366=CARTESIAN_POINT('Ctrl Pts',(-0.119609691052418,0.0523617558795304,
0.24));
#19367=CARTESIAN_POINT('Ctrl Pts',(-0.117006563775536,0.0570408964535612,
0.24));
#19368=CARTESIAN_POINT('Ctrl Pts',(-0.114113358229268,0.0615597689541448,
0.24));
#19369=CARTESIAN_POINT('Ctrl Pts',(-0.110947628485839,0.0658586917144141,
0.24));
#19370=CARTESIAN_POINT('Ctrl Pts',(-0.108265305855902,0.0695011687224882,
0.24));
#19371=CARTESIAN_POINT('Ctrl Pts',(-0.105385772272888,0.0729892759232728,
0.24));
#19372=CARTESIAN_POINT('Ctrl Pts',(-0.102309360287629,0.0763011815833395,
0.24));
#19373=CARTESIAN_POINT('Ctrl Pts',(-0.100282916666232,0.0784827457339379,
0.24));
#19374=CARTESIAN_POINT('Ctrl Pts',(-0.0981709975111385,0.0805877996091198,
0.24));
#19375=CARTESIAN_POINT('Ctrl Pts',(-0.0959791030802606,0.0826138105732947,
0.24));
#19376=CARTESIAN_POINT('Origin',(0.,0.,0.24));
#19377=CARTESIAN_POINT('',(0.158771324027147,-0.275,0.24));
#19378=CARTESIAN_POINT('',(0.317542648054294,0.,0.24));
#19379=CARTESIAN_POINT('',(0.158771324027147,-0.275,0.24));
#19380=CARTESIAN_POINT('',(0.158771324027147,0.275,0.24));
#19381=CARTESIAN_POINT('',(0.317542648054294,0.,0.24));
#19382=CARTESIAN_POINT('',(-0.158771324027147,0.275,0.24));
#19383=CARTESIAN_POINT('',(0.158771324027147,0.275,0.24));
#19384=CARTESIAN_POINT('',(-0.317542648054294,5.55111512312578E-17,0.24));
#19385=CARTESIAN_POINT('',(-0.158771324027147,0.275,0.24));
#19386=CARTESIAN_POINT('',(-0.158771324027147,-0.275,0.24));
#19387=CARTESIAN_POINT('',(-0.317542648054294,3.88877587532466E-17,0.24));
#19388=CARTESIAN_POINT('',(-0.158771324027147,-0.275,0.24));
#19389=CARTESIAN_POINT('Origin',(0.,0.,0.12));
#19390=CARTESIAN_POINT('Origin',(-0.158771324027147,-0.275,0.));
#19391=CARTESIAN_POINT('',(-0.158771324027147,-0.275,0.));
#19392=CARTESIAN_POINT('',(0.158771324027147,-0.275,0.));
#19393=CARTESIAN_POINT('',(-0.158771324027147,-0.275,0.));
#19394=CARTESIAN_POINT('',(0.158771324027147,-0.275,0.));
#19395=CARTESIAN_POINT('',(-0.158771324027147,-0.275,0.));
#19396=CARTESIAN_POINT('Origin',(-0.317542648054294,3.88877587532466E-17,
0.));
#19397=CARTESIAN_POINT('',(-0.317542648054294,3.88877587532466E-17,0.));
#19398=CARTESIAN_POINT('',(-0.317542648054294,3.88877587532466E-17,0.));
#19399=CARTESIAN_POINT('',(-0.317542648054294,3.88877587532466E-17,0.));
#19400=CARTESIAN_POINT('Origin',(-0.158771324027147,0.275,0.));
#19401=CARTESIAN_POINT('',(-0.158771324027147,0.275,0.));
#19402=CARTESIAN_POINT('',(-0.158771324027147,0.275,0.));
#19403=CARTESIAN_POINT('',(-0.158771324027147,0.275,0.));
#19404=CARTESIAN_POINT('Origin',(0.158771324027147,0.275,0.));
#19405=CARTESIAN_POINT('',(0.158771324027147,0.275,0.));
#19406=CARTESIAN_POINT('',(0.158771324027147,0.275,0.));
#19407=CARTESIAN_POINT('',(0.158771324027147,0.275,0.));
#19408=CARTESIAN_POINT('Origin',(0.317542648054294,0.,0.));
#19409=CARTESIAN_POINT('',(0.317542648054294,0.,0.));
#19410=CARTESIAN_POINT('',(0.317542648054294,0.,0.));
#19411=CARTESIAN_POINT('',(0.317542648054294,0.,0.));
#19412=CARTESIAN_POINT('Origin',(0.158771324027147,-0.275,0.));
#19413=CARTESIAN_POINT('',(0.158771324027147,-0.275,0.));
#19414=CARTESIAN_POINT('Origin',(0.,0.,0.));
#19456=UNCERTAINTY_MEASURE_WITH_UNIT(LENGTH_MEASURE(0.001),#19472,
'DISTANCE_ACCURACY_VALUE',
'Maximum model space distance between geometric entities at asserted c
onnectivities');
#19458=UNCERTAINTY_MEASURE_WITH_UNIT(LENGTH_MEASURE(0.001),#19472,
'DISTANCE_ACCURACY_VALUE',
'Maximum model space distance between geometric entities at asserted c
onnectivities');
#19469=(
GEOMETRIC_REPRESENTATION_CONTEXT(3)
GLOBAL_UNCERTAINTY_ASSIGNED_CONTEXT((#19456))
GLOBAL_UNIT_ASSIGNED_CONTEXT((#19472,#19474,#19475))
REPRESENTATION_CONTEXT('','3D')
);
#19471=(
GEOMETRIC_REPRESENTATION_CONTEXT(3)
GLOBAL_UNCERTAINTY_ASSIGNED_CONTEXT((#19458))
GLOBAL_UNIT_ASSIGNED_CONTEXT((#19472,#19474,#19475))
REPRESENTATION_CONTEXT('','3D')
);
#19472=(
LENGTH_UNIT()
NAMED_UNIT(*)
SI_UNIT(.CENTI.,.METRE.)
);
#19474=(
NAMED_UNIT(*)
PLANE_ANGLE_UNIT()
SI_UNIT($,.RADIAN.)
);
#19475=(
NAMED_UNIT(*)
SI_UNIT($,.STERADIAN.)
SOLID_ANGLE_UNIT()
);
#19486=SHAPE_DEFINITION_REPRESENTATION(#19498,#19526);
#19498=PRODUCT_DEFINITION_SHAPE('',$,#19539);
#19526=SHAPE_REPRESENTATION('',(#7768),#19469);
#19528=PRODUCT_DEFINITION_CONTEXT('part definition',#19566,'design');
#19539=PRODUCT_DEFINITION('2026-11-10-01-30-02-398','Hex nut M3',#19551,
#19528);
#19551=PRODUCT_DEFINITION_FORMATION('',$,#19578);
#19566=APPLICATION_CONTEXT(
'Core Data for Automotive Mechanical Design Process');
#19567=PRODUCT_CONTEXT('part definition',#19566,'mechanical');
#19578=PRODUCT('2026-11-10-01-30-02-398','Hex nut M3',$,(#19567));
#19586=PRESENTATION_STYLE_ASSIGNMENT((#19594));
#19594=SURFACE_STYLE_USAGE(.BOTH.,#19602);
#19602=SURFACE_SIDE_STYLE('',(#19610));
#19610=SURFACE_STYLE_FILL_AREA(#19618);
#19618=FILL_AREA_STYLE('Fastener gray',(#19626));
#19626=FILL_AREA_STYLE_COLOUR('Fastener gray',#19634);
#19634=COLOUR_RGB('Fastener gray',0.607843137254902,0.643137254901961,0.698039215686274);
ENDSEC;
END-ISO-10303-21;
